ISO-10303-21;
HEADER;
/* Generated by software containing ST-Developer
 * from STEP Tools, Inc. (www.steptools.com) 
 */

FILE_DESCRIPTION(
/* description */ ('STEP AP214'),
/* implementation_level */ '2;1');

FILE_NAME(
/* name */ 'PUR-HW-4008.step',
/* time_stamp */ '2026-10-07T12:49:37-07:00',
/* author */ (''),
/* organization */ (''),
/* preprocessor_version */ 'ST-DEVELOPER v20.2',
/* originating_system */ 'Autodesk Translation Framework v15.15.0.0',
/* authorisation */ '');

FILE_SCHEMA (('AUTOMOTIVE_DESIGN { 1 0 10303 214 3 1 1 }'));
ENDSEC;

DATA;
#10=MECHANICAL_DESIGN_GEOMETRIC_PRESENTATION_REPRESENTATION('',(#293),#33016);
#196=(
BOUNDED_CURVE()
B_SPLINE_CURVE(2,(#19890,#19891,#19892,#19893,#19894,#19895,#19896,#19897,
#19898,#19899,#19900,#19901,#19902),.UNSPECIFIED.,.F.,.F.)
B_SPLINE_CURVE_WITH_KNOTS((3,2,2,2,2,2,3),(0.833333333333333,0.861111111111111,
0.888888888888889,0.916666666666667,0.944444444444444,0.972222222222222,
1.),.UNSPECIFIED.)
CURVE()
GEOMETRIC_REPRESENTATION_ITEM()
RATIONAL_B_SPLINE_CURVE((1.,0.866025403784439,1.,0.866025403784439,1.,0.866025403784439,
1.,0.866025403784439,1.,0.866025403784439,1.,0.866025403784439,1.))
REPRESENTATION_ITEM('')
);
#197=(
BOUNDED_CURVE()
B_SPLINE_CURVE(2,(#19904,#19905,#19906,#19907,#19908,#19909,#19910,#19911,
#19912,#19913,#19914,#19915,#19916,#19917,#19918,#19919,#19920,#19921,#19922,
#19923,#19924,#19925,#19926,#19927,#19928,#19929,#19930,#19931,#19932,#19933,
#19934,#19935,#19936,#19937,#19938,#19939,#19940,#19941,#19942,#19943,#19944,
#19945,#19946,#19947,#19948,#19949,#19950,#19951,#19952,#19953,#19954,#19955,
#19956,#19957,#19958,#19959,#19960,#19961,#19962,#19963,#19964),
 .UNSPECIFIED.,.F.,.F.)
B_SPLINE_CURVE_WITH_KNOTS((3,2,2,2,2,2,2,2,2,2,2,2,2,2,2,2,2,2,2,2,2,2,
2,2,2,2,2,2,2,2,3),(0.,0.0277777777777778,0.0555555555555556,0.0833333333333333,
0.111111111111111,0.138888888888889,0.166666666666667,0.194444444444444,
0.222222222222222,0.25,0.277777777777778,0.305555555555556,0.333333333333333,
0.361111111111111,0.388888888888889,0.416666666666667,0.444444444444444,
0.472222222222222,0.5,0.527777777777778,0.555555555555556,0.583333333333333,
0.611111111111111,0.638888888888889,0.666666666666667,0.694444444444444,
0.722222222222222,0.75,0.777777777777778,0.805555555555556,0.833333333333333),
 .UNSPECIFIED.)
CURVE()
GEOMETRIC_REPRESENTATION_ITEM()
RATIONAL_B_SPLINE_CURVE((1.,0.866025403784439,1.,0.866025403784439,1.,0.866025403784439,
1.,0.866025403784439,1.,0.866025403784439,1.,0.866025403784439,1.,0.866025403784439,
1.,0.866025403784439,1.,0.866025403784439,1.,0.866025403784439,1.,0.866025403784439,
1.,0.866025403784439,1.,0.866025403784439,1.,0.866025403784439,1.,0.866025403784439,
1.,0.866025403784439,1.,0.866025403784439,1.,0.866025403784439,1.,0.866025403784439,
1.,0.866025403784439,1.,0.866025403784439,1.,0.866025403784439,1.,0.866025403784439,
1.,0.866025403784439,1.,0.866025403784439,1.,0.866025403784439,1.,0.866025403784439,
1.,0.866025403784439,1.,0.866025403784439,1.,0.866025403784439,1.))
REPRESENTATION_ITEM('')
);
#198=(
BOUNDED_CURVE()
B_SPLINE_CURVE(2,(#19967,#19968,#19969,#19970,#19971,#19972,#19973,#19974,
#19975,#19976,#19977,#19978,#19979,#19980,#19981,#19982,#19983,#19984,#19985,
#19986,#19987,#19988,#19989,#19990,#19991,#19992,#19993,#19994,#19995,#19996,
#19997,#19998,#19999,#20000,#20001,#20002,#20003,#20004,#20005,#20006,#20007,
#20008,#20009,#20010,#20011,#20012,#20013,#20014,#20015,#20016,#20017,#20018,
#20019,#20020,#20021,#20022,#20023,#20024,#20025,#20026,#20027,#20028,#20029,
#20030,#20031,#20032,#20033,#20034,#20035,#20036,#20037,#20038,#20039),
 .UNSPECIFIED.,.F.,.F.)
B_SPLINE_CURVE_WITH_KNOTS((3,2,2,2,2,2,2,2,2,2,2,2,2,2,2,2,2,2,2,2,2,2,
2,2,2,2,2,2,2,2,2,2,2,2,2,2,3),(0.,0.0277777777777778,0.0555555555555556,
0.0833333333333333,0.111111111111111,0.138888888888889,0.166666666666667,
0.194444444444444,0.222222222222222,0.25,0.277777777777778,0.305555555555556,
0.333333333333333,0.361111111111111,0.388888888888889,0.416666666666667,
0.444444444444444,0.472222222222222,0.5,0.527777777777778,0.555555555555556,
0.583333333333333,0.611111111111111,0.638888888888889,0.666666666666667,
0.694444444444444,0.722222222222222,0.75,0.777777777777778,0.805555555555556,
0.833333333333333,0.861111111111111,0.888888888888889,0.916666666666667,
0.944444444444444,0.972222222222222,1.),.UNSPECIFIED.)
CURVE()
GEOMETRIC_REPRESENTATION_ITEM()
RATIONAL_B_SPLINE_CURVE((1.,0.866025403784439,1.,0.866025403784439,1.,0.866025403784439,
1.,0.866025403784439,1.,0.866025403784439,1.,0.866025403784439,1.,0.866025403784439,
1.,0.866025403784439,1.,0.866025403784439,1.,0.866025403784439,1.,0.866025403784439,
1.,0.866025403784439,1.,0.866025403784439,1.,0.866025403784439,1.,0.866025403784439,
1.,0.866025403784439,1.,0.866025403784439,1.,0.866025403784439,1.,0.866025403784439,
1.,0.866025403784439,1.,0.866025403784439,1.,0.866025403784439,1.,0.866025403784439,
1.,0.866025403784439,1.,0.866025403784439,1.,0.866025403784439,1.,0.866025403784439,
1.,0.866025403784439,1.,0.866025403784439,1.,0.866025403784439,1.,0.866025403784439,
1.,0.866025403784439,1.,0.866025403784439,1.,0.866025403784439,1.,0.866025403784439,
1.,0.866025403784439,1.))
REPRESENTATION_ITEM('')
);
#199=(
BOUNDED_CURVE()
B_SPLINE_CURVE(2,(#20334,#20335,#20336,#20337,#20338,#20339,#20340,#20341,
#20342,#20343,#20344,#20345,#20346),.UNSPECIFIED.,.F.,.F.)
B_SPLINE_CURVE_WITH_KNOTS((3,2,2,2,2,2,3),(0.,0.0277777777777778,0.0555555555555556,
0.0833333333333333,0.111111111111111,0.138888888888889,0.166666666666667),
 .UNSPECIFIED.)
CURVE()
GEOMETRIC_REPRESENTATION_ITEM()
RATIONAL_B_SPLINE_CURVE((1.,0.866025403784439,1.,0.866025403784439,1.,0.866025403784439,
1.,0.866025403784439,1.,0.866025403784439,1.,0.866025403784439,1.))
REPRESENTATION_ITEM('')
);
#200=(
BOUNDED_CURVE()
B_SPLINE_CURVE(2,(#20347,#20348,#20349,#20350,#20351,#20352,#20353,#20354,
#20355,#20356,#20357,#20358,#20359,#20360,#20361,#20362,#20363,#20364,#20365,
#20366,#20367,#20368,#20369,#20370,#20371,#20372,#20373,#20374,#20375,#20376,
#20377,#20378,#20379,#20380,#20381,#20382,#20383,#20384,#20385,#20386,#20387,
#20388,#20389,#20390,#20391,#20392,#20393,#20394,#20395,#20396,#20397,#20398,
#20399,#20400,#20401,#20402,#20403,#20404,#20405,#20406,#20407),
 .UNSPECIFIED.,.F.,.F.)
B_SPLINE_CURVE_WITH_KNOTS((3,2,2,2,2,2,2,2,2,2,2,2,2,2,2,2,2,2,2,2,2,2,
2,2,2,2,2,2,2,2,3),(0.,0.0277777777777778,0.0555555555555556,0.0833333333333333,
0.111111111111111,0.138888888888889,0.166666666666667,0.194444444444444,
0.222222222222222,0.25,0.277777777777778,0.305555555555556,0.333333333333333,
0.361111111111111,0.388888888888889,0.416666666666667,0.444444444444444,
0.472222222222222,0.5,0.527777777777778,0.555555555555556,0.583333333333333,
0.611111111111111,0.638888888888889,0.666666666666667,0.694444444444444,
0.722222222222222,0.75,0.777777777777778,0.805555555555556,0.833333333333333),
 .UNSPECIFIED.)
CURVE()
GEOMETRIC_REPRESENTATION_ITEM()
RATIONAL_B_SPLINE_CURVE((1.,0.866025403784439,1.,0.866025403784439,1.,0.866025403784439,
1.,0.866025403784439,1.,0.866025403784439,1.,0.866025403784439,1.,0.866025403784439,
1.,0.866025403784439,1.,0.866025403784439,1.,0.866025403784439,1.,0.866025403784439,
1.,0.866025403784439,1.,0.866025403784439,1.,0.866025403784439,1.,0.866025403784439,
1.,0.866025403784439,1.,0.866025403784439,1.,0.866025403784439,1.,0.866025403784439,
1.,0.866025403784439,1.,0.866025403784439,1.,0.866025403784439,1.,0.866025403784439,
1.,0.866025403784439,1.,0.866025403784439,1.,0.866025403784439,1.,0.866025403784439,
1.,0.866025403784439,1.,0.866025403784439,1.,0.866025403784439,1.))
REPRESENTATION_ITEM('')
);
#201=(
BOUNDED_CURVE()
B_SPLINE_CURVE(2,(#20704,#20705,#20706,#20707,#20708,#20709,#20710,#20711,
#20712,#20713,#20714,#20715,#20716,#20717,#20718,#20719,#20720,#20721,#20722,
#20723,#20724,#20725,#20726,#20727,#20728,#20729,#20730,#20731,#20732,#20733,
#20734,#20735,#20736,#20737,#20738,#20739,#20740,#20741,#20742,#20743,#20744,
#20745,#20746,#20747,#20748,#20749,#20750,#20751,#20752,#20753,#20754,#20755,
#20756,#20757,#20758,#20759,#20760,#20761,#20762,#20763,#20764,#20765,#20766,
#20767,#20768,#20769,#20770,#20771,#20772,#20773,#20774,#20775,#20776),
 .UNSPECIFIED.,.F.,.F.)
B_SPLINE_CURVE_WITH_KNOTS((3,2,2,2,2,2,2,2,2,2,2,2,2,2,2,2,2,2,2,2,2,2,
2,2,2,2,2,2,2,2,2,2,2,2,2,2,3),(0.,0.0277777777777778,0.0555555555555556,
0.0833333333333333,0.111111111111111,0.138888888888889,0.166666666666667,
0.194444444444444,0.222222222222222,0.25,0.277777777777778,0.305555555555556,
0.333333333333333,0.361111111111111,0.388888888888889,0.416666666666667,
0.444444444444444,0.472222222222222,0.5,0.527777777777778,0.555555555555556,
0.583333333333333,0.611111111111111,0.638888888888889,0.666666666666667,
0.694444444444444,0.722222222222222,0.75,0.777777777777778,0.805555555555556,
0.833333333333333,0.861111111111111,0.888888888888889,0.916666666666667,
0.944444444444444,0.972222222222222,1.),.UNSPECIFIED.)
CURVE()
GEOMETRIC_REPRESENTATION_ITEM()
RATIONAL_B_SPLINE_CURVE((1.,0.866025403784439,1.,0.866025403784439,1.,0.866025403784439,
1.,0.866025403784439,1.,0.866025403784439,1.,0.866025403784439,1.,0.866025403784439,
1.,0.866025403784439,1.,0.866025403784439,1.,0.866025403784439,1.,0.866025403784439,
1.,0.866025403784439,1.,0.866025403784439,1.,0.866025403784439,1.,0.866025403784439,
1.,0.866025403784439,1.,0.866025403784439,1.,0.866025403784439,1.,0.866025403784439,
1.,0.866025403784439,1.,0.866025403784439,1.,0.866025403784439,1.,0.866025403784439,
1.,0.866025403784439,1.,0.866025403784439,1.,0.866025403784439,1.,0.866025403784439,
1.,0.866025403784439,1.,0.866025403784439,1.,0.866025403784439,1.,0.866025403784439,
1.,0.866025403784439,1.,0.866025403784439,1.,0.866025403784439,1.,0.866025403784439,
1.,0.866025403784439,1.))
REPRESENTATION_ITEM('')
);
#239=SHAPE_REPRESENTATION_RELATIONSHIP('SRR','None',#33132,#266);
#266=ADVANCED_BREP_SHAPE_REPRESENTATION('',(#324),#32993);
#293=STYLED_ITEM('',(#33285),#324);
#324=MANIFOLD_SOLID_BREP('Body1',#9948);
#435=(
BOUNDED_SURFACE()
B_SPLINE_SURFACE(3,2,((#19594,#19595,#19596,#19597,#19598,#19599,#19600,
#19601,#19602,#19603,#19604,#19605,#19606,#19607,#19608,#19609,#19610,#19611,
#19612,#19613,#19614,#19615,#19616,#19617,#19618,#19619,#19620,#19621,#19622,
#19623,#19624,#19625,#19626,#19627,#19628,#19629,#19630,#19631,#19632,#19633,
#19634,#19635,#19636,#19637,#19638,#19639,#19640,#19641,#19642,#19643,#19644,
#19645,#19646,#19647,#19648,#19649,#19650,#19651,#19652,#19653,#19654,#19655,
#19656,#19657,#19658,#19659,#19660,#19661,#19662,#19663,#19664,#19665,#19666),
(#19667,#19668,#19669,#19670,#19671,#19672,#19673,#19674,#19675,#19676,
#19677,#19678,#19679,#19680,#19681,#19682,#19683,#19684,#19685,#19686,#19687,
#19688,#19689,#19690,#19691,#19692,#19693,#19694,#19695,#19696,#19697,#19698,
#19699,#19700,#19701,#19702,#19703,#19704,#19705,#19706,#19707,#19708,#19709,
#19710,#19711,#19712,#19713,#19714,#19715,#19716,#19717,#19718,#19719,#19720,
#19721,#19722,#19723,#19724,#19725,#19726,#19727,#19728,#19729,#19730,#19731,
#19732,#19733,#19734,#19735,#19736,#19737,#19738,#19739),(#19740,#19741,
#19742,#19743,#19744,#19745,#19746,#19747,#19748,#19749,#19750,#19751,#19752,
#19753,#19754,#19755,#19756,#19757,#19758,#19759,#19760,#19761,#19762,#19763,
#19764,#19765,#19766,#19767,#19768,#19769,#19770,#19771,#19772,#19773,#19774,
#19775,#19776,#19777,#19778,#19779,#19780,#19781,#19782,#19783,#19784,#19785,
#19786,#19787,#19788,#19789,#19790,#19791,#19792,#19793,#19794,#19795,#19796,
#19797,#19798,#19799,#19800,#19801,#19802,#19803,#19804,#19805,#19806,#19807,
#19808,#19809,#19810,#19811,#19812),(#19813,#19814,#19815,#19816,#19817,
#19818,#19819,#19820,#19821,#19822,#19823,#19824,#19825,#19826,#19827,#19828,
#19829,#19830,#19831,#19832,#19833,#19834,#19835,#19836,#19837,#19838,#19839,
#19840,#19841,#19842,#19843,#19844,#19845,#19846,#19847,#19848,#19849,#19850,
#19851,#19852,#19853,#19854,#19855,#19856,#19857,#19858,#19859,#19860,#19861,
#19862,#19863,#19864,#19865,#19866,#19867,#19868,#19869,#19870,#19871,#19872,
#19873,#19874,#19875,#19876,#19877,#19878,#19879,#19880,#19881,#19882,#19883,
#19884,#19885)),.UNSPECIFIED.,.F.,.F.,.F.)
B_SPLINE_SURFACE_WITH_KNOTS((4,4),(3,2,2,2,2,2,2,2,2,2,2,2,2,2,2,2,2,2,
2,2,2,2,2,2,2,2,2,2,2,2,2,2,2,2,2,2,3),(0.,1.),(0.,0.0277777777777778,0.0555555555555556,
0.0833333333333333,0.111111111111111,0.138888888888889,0.166666666666667,
0.194444444444444,0.222222222222222,0.25,0.277777777777778,0.305555555555556,
0.333333333333333,0.361111111111111,0.388888888888889,0.416666666666667,
0.444444444444444,0.472222222222222,0.5,0.527777777777778,0.555555555555556,
0.583333333333333,0.611111111111111,0.638888888888889,0.666666666666667,
0.694444444444444,0.722222222222222,0.75,0.777777777777778,0.805555555555556,
0.833333333333333,0.861111111111111,0.888888888888889,0.916666666666667,
0.944444444444444,0.972222222222222,1.),.UNSPECIFIED.)
GEOMETRIC_REPRESENTATION_ITEM()
RATIONAL_B_SPLINE_SURFACE(((1.,0.866025403784439,1.,0.866025403784439,1.,
0.866025403784439,1.,0.866025403784439,1.,0.866025403784439,1.,0.866025403784439,
1.,0.866025403784439,1.,0.866025403784439,1.,0.866025403784439,1.,0.866025403784439,
1.,0.866025403784439,1.,0.866025403784439,1.,0.866025403784439,1.,0.866025403784439,
1.,0.866025403784439,1.,0.866025403784439,1.,0.866025403784439,1.,0.866025403784439,
1.,0.866025403784439,1.,0.866025403784439,1.,0.866025403784439,1.,0.866025403784439,
1.,0.866025403784439,1.,0.866025403784439,1.,0.866025403784439,1.,0.866025403784439,
1.,0.866025403784439,1.,0.866025403784439,1.,0.866025403784439,1.,0.866025403784439,
1.,0.866025403784439,1.,0.866025403784439,1.,0.866025403784439,1.,0.866025403784439,
1.,0.866025403784439,1.,0.866025403784439,1.),(0.804737854124365,0.696923425058676,
0.804737854124365,0.696923425058676,0.804737854124365,0.696923425058676,
0.804737854124365,0.696923425058676,0.804737854124365,0.696923425058676,
0.804737854124365,0.696923425058676,0.804737854124365,0.696923425058676,
0.804737854124365,0.696923425058676,0.804737854124365,0.696923425058676,
0.804737854124365,0.696923425058676,0.804737854124365,0.696923425058676,
0.804737854124365,0.696923425058676,0.804737854124365,0.696923425058676,
0.804737854124365,0.696923425058676,0.804737854124365,0.696923425058676,
0.804737854124365,0.696923425058676,0.804737854124365,0.696923425058676,
0.804737854124365,0.696923425058676,0.804737854124365,0.696923425058676,
0.804737854124365,0.696923425058676,0.804737854124365,0.696923425058676,
0.804737854124365,0.696923425058676,0.804737854124365,0.696923425058676,
0.804737854124365,0.696923425058676,0.804737854124365,0.696923425058676,
0.804737854124365,0.696923425058676,0.804737854124365,0.696923425058676,
0.804737854124365,0.696923425058676,0.804737854124365,0.696923425058676,
0.804737854124365,0.696923425058676,0.804737854124365,0.696923425058676,
0.804737854124365,0.696923425058676,0.804737854124365,0.696923425058676,
0.804737854124365,0.696923425058676,0.804737854124365,0.696923425058676,
0.804737854124365,0.696923425058676,0.804737854124365),(0.804737854124365,
0.696923425058676,0.804737854124365,0.696923425058676,0.804737854124365,
0.696923425058676,0.804737854124365,0.696923425058676,0.804737854124365,
0.696923425058676,0.804737854124365,0.696923425058676,0.804737854124365,
0.696923425058676,0.804737854124365,0.696923425058676,0.804737854124365,
0.696923425058676,0.804737854124365,0.696923425058676,0.804737854124365,
0.696923425058676,0.804737854124365,0.696923425058676,0.804737854124365,
0.696923425058676,0.804737854124365,0.696923425058676,0.804737854124365,
0.696923425058676,0.804737854124365,0.696923425058676,0.804737854124365,
0.696923425058676,0.804737854124365,0.696923425058676,0.804737854124365,
0.696923425058676,0.804737854124365,0.696923425058676,0.804737854124365,
0.696923425058676,0.804737854124365,0.696923425058676,0.804737854124365,
0.696923425058676,0.804737854124365,0.696923425058676,0.804737854124365,
0.696923425058676,0.804737854124365,0.696923425058676,0.804737854124365,
0.696923425058676,0.804737854124365,0.696923425058676,0.804737854124365,
0.696923425058676,0.804737854124365,0.696923425058676,0.804737854124365,
0.696923425058676,0.804737854124365,0.696923425058676,0.804737854124365,
0.696923425058676,0.804737854124365,0.696923425058676,0.804737854124365,
0.696923425058676,0.804737854124365,0.696923425058676,0.804737854124365),
(1.,0.866025403784439,1.,0.866025403784439,1.,0.866025403784439,1.,0.866025403784439,
1.,0.866025403784439,1.,0.866025403784439,1.,0.866025403784439,1.,0.866025403784439,
1.,0.866025403784439,1.,0.866025403784439,1.,0.866025403784439,1.,0.866025403784439,
1.,0.866025403784439,1.,0.866025403784439,1.,0.866025403784439,1.,0.866025403784439,
1.,0.866025403784439,1.,0.866025403784439,1.,0.866025403784439,1.,0.866025403784439,
1.,0.866025403784439,1.,0.866025403784439,1.,0.866025403784439,1.,0.866025403784439,
1.,0.866025403784439,1.,0.866025403784439,1.,0.866025403784439,1.,0.866025403784439,
1.,0.866025403784439,1.,0.866025403784439,1.,0.866025403784439,1.,0.866025403784439,
1.,0.866025403784439,1.,0.866025403784439,1.,0.866025403784439,1.,0.866025403784439,
1.)))
REPRESENTATION_ITEM('')
SURFACE()
);
#436=(
BOUNDED_SURFACE()
B_SPLINE_SURFACE(3,2,((#20040,#20041,#20042,#20043,#20044,#20045,#20046,
#20047,#20048,#20049,#20050,#20051,#20052,#20053,#20054,#20055,#20056,#20057,
#20058,#20059,#20060,#20061,#20062,#20063,#20064,#20065,#20066,#20067,#20068,
#20069,#20070,#20071,#20072,#20073,#20074,#20075,#20076,#20077,#20078,#20079,
#20080,#20081,#20082,#20083,#20084,#20085,#20086,#20087,#20088,#20089,#20090,
#20091,#20092,#20093,#20094,#20095,#20096,#20097,#20098,#20099,#20100,#20101,
#20102,#20103,#20104,#20105,#20106,#20107,#20108,#20109,#20110,#20111,#20112),
(#20113,#20114,#20115,#20116,#20117,#20118,#20119,#20120,#20121,#20122,
#20123,#20124,#20125,#20126,#20127,#20128,#20129,#20130,#20131,#20132,#20133,
#20134,#20135,#20136,#20137,#20138,#20139,#20140,#20141,#20142,#20143,#20144,
#20145,#20146,#20147,#20148,#20149,#20150,#20151,#20152,#20153,#20154,#20155,
#20156,#20157,#20158,#20159,#20160,#20161,#20162,#20163,#20164,#20165,#20166,
#20167,#20168,#20169,#20170,#20171,#20172,#20173,#20174,#20175,#20176,#20177,
#20178,#20179,#20180,#20181,#20182,#20183,#20184,#20185),(#20186,#20187,
#20188,#20189,#20190,#20191,#20192,#20193,#20194,#20195,#20196,#20197,#20198,
#20199,#20200,#20201,#20202,#20203,#20204,#20205,#20206,#20207,#20208,#20209,
#20210,#20211,#20212,#20213,#20214,#20215,#20216,#20217,#20218,#20219,#20220,
#20221,#20222,#20223,#20224,#20225,#20226,#20227,#20228,#20229,#20230,#20231,
#20232,#20233,#20234,#20235,#20236,#20237,#20238,#20239,#20240,#20241,#20242,
#20243,#20244,#20245,#20246,#20247,#20248,#20249,#20250,#20251,#20252,#20253,
#20254,#20255,#20256,#20257,#20258),(#20259,#20260,#20261,#20262,#20263,
#20264,#20265,#20266,#20267,#20268,#20269,#20270,#20271,#20272,#20273,#20274,
#20275,#20276,#20277,#20278,#20279,#20280,#20281,#20282,#20283,#20284,#20285,
#20286,#20287,#20288,#20289,#20290,#20291,#20292,#20293,#20294,#20295,#20296,
#20297,#20298,#20299,#20300,#20301,#20302,#20303,#20304,#20305,#20306,#20307,
#20308,#20309,#20310,#20311,#20312,#20313,#20314,#20315,#20316,#20317,#20318,
#20319,#20320,#20321,#20322,#20323,#20324,#20325,#20326,#20327,#20328,#20329,
#20330,#20331)),.UNSPECIFIED.,.F.,.F.,.F.)
B_SPLINE_SURFACE_WITH_KNOTS((4,4),(3,2,2,2,2,2,2,2,2,2,2,2,2,2,2,2,2,2,
2,2,2,2,2,2,2,2,2,2,2,2,2,2,2,2,2,2,3),(0.,1.),(0.,0.0277777777777778,0.0555555555555556,
0.0833333333333333,0.111111111111111,0.138888888888889,0.166666666666667,
0.194444444444444,0.222222222222222,0.25,0.277777777777778,0.305555555555556,
0.333333333333333,0.361111111111111,0.388888888888889,0.416666666666667,
0.444444444444444,0.472222222222222,0.5,0.527777777777778,0.555555555555556,
0.583333333333333,0.611111111111111,0.638888888888889,0.666666666666667,
0.694444444444444,0.722222222222222,0.75,0.777777777777778,0.805555555555556,
0.833333333333333,0.861111111111111,0.888888888888889,0.916666666666667,
0.944444444444444,0.972222222222222,1.),.UNSPECIFIED.)
GEOMETRIC_REPRESENTATION_ITEM()
RATIONAL_B_SPLINE_SURFACE(((1.,0.866025403784439,1.,0.866025403784439,1.,
0.866025403784439,1.,0.866025403784439,1.,0.866025403784439,1.,0.866025403784439,
1.,0.866025403784439,1.,0.866025403784439,1.,0.866025403784439,1.,0.866025403784439,
1.,0.866025403784439,1.,0.866025403784439,1.,0.866025403784439,1.,0.866025403784439,
1.,0.866025403784439,1.,0.866025403784439,1.,0.866025403784439,1.,0.866025403784439,
1.,0.866025403784439,1.,0.866025403784439,1.,0.866025403784439,1.,0.866025403784439,
1.,0.866025403784439,1.,0.866025403784439,1.,0.866025403784439,1.,0.866025403784439,
1.,0.866025403784439,1.,0.866025403784439,1.,0.866025403784439,1.,0.866025403784439,
1.,0.866025403784439,1.,0.866025403784439,1.,0.866025403784439,1.,0.866025403784439,
1.,0.866025403784439,1.,0.866025403784439,1.),(0.804737854124365,0.696923425058676,
0.804737854124365,0.696923425058676,0.804737854124365,0.696923425058676,
0.804737854124365,0.696923425058676,0.804737854124365,0.696923425058676,
0.804737854124365,0.696923425058676,0.804737854124365,0.696923425058676,
0.804737854124365,0.696923425058676,0.804737854124365,0.696923425058676,
0.804737854124365,0.696923425058676,0.804737854124365,0.696923425058676,
0.804737854124365,0.696923425058676,0.804737854124365,0.696923425058676,
0.804737854124365,0.696923425058676,0.804737854124365,0.696923425058676,
0.804737854124365,0.696923425058676,0.804737854124365,0.696923425058676,
0.804737854124365,0.696923425058676,0.804737854124365,0.696923425058676,
0.804737854124365,0.696923425058676,0.804737854124365,0.696923425058676,
0.804737854124365,0.696923425058676,0.804737854124365,0.696923425058676,
0.804737854124365,0.696923425058676,0.804737854124365,0.696923425058676,
0.804737854124365,0.696923425058676,0.804737854124365,0.696923425058676,
0.804737854124365,0.696923425058676,0.804737854124365,0.696923425058676,
0.804737854124365,0.696923425058676,0.804737854124365,0.696923425058676,
0.804737854124365,0.696923425058676,0.804737854124365,0.696923425058676,
0.804737854124365,0.696923425058676,0.804737854124365,0.696923425058676,
0.804737854124365,0.696923425058676,0.804737854124365),(0.804737854124365,
0.696923425058676,0.804737854124365,0.696923425058676,0.804737854124365,
0.696923425058676,0.804737854124365,0.696923425058676,0.804737854124365,
0.696923425058676,0.804737854124365,0.696923425058676,0.804737854124365,
0.696923425058676,0.804737854124365,0.696923425058676,0.804737854124365,
0.696923425058676,0.804737854124365,0.696923425058676,0.804737854124365,
0.696923425058676,0.804737854124365,0.696923425058676,0.804737854124365,
0.696923425058676,0.804737854124365,0.696923425058676,0.804737854124365,
0.696923425058676,0.804737854124365,0.696923425058676,0.804737854124365,
0.696923425058676,0.804737854124365,0.696923425058676,0.804737854124365,
0.696923425058676,0.804737854124365,0.696923425058676,0.804737854124365,
0.696923425058676,0.804737854124365,0.696923425058676,0.804737854124365,
0.696923425058676,0.804737854124365,0.696923425058676,0.804737854124365,
0.696923425058676,0.804737854124365,0.696923425058676,0.804737854124365,
0.696923425058676,0.804737854124365,0.696923425058676,0.804737854124365,
0.696923425058676,0.804737854124365,0.696923425058676,0.804737854124365,
0.696923425058676,0.804737854124365,0.696923425058676,0.804737854124365,
0.696923425058676,0.804737854124365,0.696923425058676,0.804737854124365,
0.696923425058676,0.804737854124365,0.696923425058676,0.804737854124365),
(1.,0.866025403784439,1.,0.866025403784439,1.,0.866025403784439,1.,0.866025403784439,
1.,0.866025403784439,1.,0.866025403784439,1.,0.866025403784439,1.,0.866025403784439,
1.,0.866025403784439,1.,0.866025403784439,1.,0.866025403784439,1.,0.866025403784439,
1.,0.866025403784439,1.,0.866025403784439,1.,0.866025403784439,1.,0.866025403784439,
1.,0.866025403784439,1.,0.866025403784439,1.,0.866025403784439,1.,0.866025403784439,
1.,0.866025403784439,1.,0.866025403784439,1.,0.866025403784439,1.,0.866025403784439,
1.,0.866025403784439,1.,0.866025403784439,1.,0.866025403784439,1.,0.866025403784439,
1.,0.866025403784439,1.,0.866025403784439,1.,0.866025403784439,1.,0.866025403784439,
1.,0.866025403784439,1.,0.866025403784439,1.,0.866025403784439,1.,0.866025403784439,
1.)))
REPRESENTATION_ITEM('')
SURFACE()
);
#437=(
BOUNDED_SURFACE()
B_SPLINE_SURFACE(3,2,((#20409,#20410,#20411,#20412,#20413,#20414,#20415,
#20416,#20417,#20418,#20419,#20420,#20421,#20422,#20423,#20424,#20425,#20426,
#20427,#20428,#20429,#20430,#20431,#20432,#20433,#20434,#20435,#20436,#20437,
#20438,#20439,#20440,#20441,#20442,#20443,#20444,#20445,#20446,#20447,#20448,
#20449,#20450,#20451,#20452,#20453,#20454,#20455,#20456,#20457,#20458,#20459,
#20460,#20461,#20462,#20463,#20464,#20465,#20466,#20467,#20468,#20469,#20470,
#20471,#20472,#20473,#20474,#20475,#20476,#20477,#20478,#20479,#20480,#20481),
(#20482,#20483,#20484,#20485,#20486,#20487,#20488,#20489,#20490,#20491,
#20492,#20493,#20494,#20495,#20496,#20497,#20498,#20499,#20500,#20501,#20502,
#20503,#20504,#20505,#20506,#20507,#20508,#20509,#20510,#20511,#20512,#20513,
#20514,#20515,#20516,#20517,#20518,#20519,#20520,#20521,#20522,#20523,#20524,
#20525,#20526,#20527,#20528,#20529,#20530,#20531,#20532,#20533,#20534,#20535,
#20536,#20537,#20538,#20539,#20540,#20541,#20542,#20543,#20544,#20545,#20546,
#20547,#20548,#20549,#20550,#20551,#20552,#20553,#20554),(#20555,#20556,
#20557,#20558,#20559,#20560,#20561,#20562,#20563,#20564,#20565,#20566,#20567,
#20568,#20569,#20570,#20571,#20572,#20573,#20574,#20575,#20576,#20577,#20578,
#20579,#20580,#20581,#20582,#20583,#20584,#20585,#20586,#20587,#20588,#20589,
#20590,#20591,#20592,#20593,#20594,#20595,#20596,#20597,#20598,#20599,#20600,
#20601,#20602,#20603,#20604,#20605,#20606,#20607,#20608,#20609,#20610,#20611,
#20612,#20613,#20614,#20615,#20616,#20617,#20618,#20619,#20620,#20621,#20622,
#20623,#20624,#20625,#20626,#20627),(#20628,#20629,#20630,#20631,#20632,
#20633,#20634,#20635,#20636,#20637,#20638,#20639,#20640,#20641,#20642,#20643,
#20644,#20645,#20646,#20647,#20648,#20649,#20650,#20651,#20652,#20653,#20654,
#20655,#20656,#20657,#20658,#20659,#20660,#20661,#20662,#20663,#20664,#20665,
#20666,#20667,#20668,#20669,#20670,#20671,#20672,#20673,#20674,#20675,#20676,
#20677,#20678,#20679,#20680,#20681,#20682,#20683,#20684,#20685,#20686,#20687,
#20688,#20689,#20690,#20691,#20692,#20693,#20694,#20695,#20696,#20697,#20698,
#20699,#20700)),.UNSPECIFIED.,.F.,.F.,.F.)
B_SPLINE_SURFACE_WITH_KNOTS((4,4),(3,2,2,2,2,2,2,2,2,2,2,2,2,2,2,2,2,2,
2,2,2,2,2,2,2,2,2,2,2,2,2,2,2,2,2,2,3),(0.,1.),(0.,0.0277777777777778,0.0555555555555556,
0.0833333333333333,0.111111111111111,0.138888888888889,0.166666666666667,
0.194444444444444,0.222222222222222,0.25,0.277777777777778,0.305555555555556,
0.333333333333333,0.361111111111111,0.388888888888889,0.416666666666667,
0.444444444444444,0.472222222222222,0.5,0.527777777777778,0.555555555555556,
0.583333333333333,0.611111111111111,0.638888888888889,0.666666666666667,
0.694444444444444,0.722222222222222,0.75,0.777777777777778,0.805555555555556,
0.833333333333333,0.861111111111111,0.888888888888889,0.916666666666667,
0.944444444444444,0.972222222222222,1.),.UNSPECIFIED.)
GEOMETRIC_REPRESENTATION_ITEM()
RATIONAL_B_SPLINE_SURFACE(((1.,0.866025403784439,1.,0.866025403784439,1.,
0.866025403784439,1.,0.866025403784439,1.,0.866025403784439,1.,0.866025403784439,
1.,0.866025403784439,1.,0.866025403784439,1.,0.866025403784439,1.,0.866025403784439,
1.,0.866025403784439,1.,0.866025403784439,1.,0.866025403784439,1.,0.866025403784439,
1.,0.866025403784439,1.,0.866025403784439,1.,0.866025403784439,1.,0.866025403784439,
1.,0.866025403784439,1.,0.866025403784439,1.,0.866025403784439,1.,0.866025403784439,
1.,0.866025403784439,1.,0.866025403784439,1.,0.866025403784439,1.,0.866025403784439,
1.,0.866025403784439,1.,0.866025403784439,1.,0.866025403784439,1.,0.866025403784439,
1.,0.866025403784439,1.,0.866025403784439,1.,0.866025403784439,1.,0.866025403784439,
1.,0.866025403784439,1.,0.866025403784439,1.),(0.804737854124365,0.696923425058676,
0.804737854124365,0.696923425058676,0.804737854124365,0.696923425058676,
0.804737854124365,0.696923425058676,0.804737854124365,0.696923425058676,
0.804737854124365,0.696923425058676,0.804737854124365,0.696923425058676,
0.804737854124365,0.696923425058676,0.804737854124365,0.696923425058676,
0.804737854124365,0.696923425058676,0.804737854124365,0.696923425058676,
0.804737854124365,0.696923425058676,0.804737854124365,0.696923425058676,
0.804737854124365,0.696923425058676,0.804737854124365,0.696923425058676,
0.804737854124365,0.696923425058676,0.804737854124365,0.696923425058676,
0.804737854124365,0.696923425058676,0.804737854124365,0.696923425058676,
0.804737854124365,0.696923425058676,0.804737854124365,0.696923425058676,
0.804737854124365,0.696923425058676,0.804737854124365,0.696923425058676,
0.804737854124365,0.696923425058676,0.804737854124365,0.696923425058676,
0.804737854124365,0.696923425058676,0.804737854124365,0.696923425058676,
0.804737854124365,0.696923425058676,0.804737854124365,0.696923425058676,
0.804737854124365,0.696923425058676,0.804737854124365,0.696923425058676,
0.804737854124365,0.696923425058676,0.804737854124365,0.696923425058676,
0.804737854124365,0.696923425058676,0.804737854124365,0.696923425058676,
0.804737854124365,0.696923425058676,0.804737854124365),(0.804737854124365,
0.696923425058676,0.804737854124365,0.696923425058676,0.804737854124365,
0.696923425058676,0.804737854124365,0.696923425058676,0.804737854124365,
0.696923425058676,0.804737854124365,0.696923425058676,0.804737854124365,
0.696923425058676,0.804737854124365,0.696923425058676,0.804737854124365,
0.696923425058676,0.804737854124365,0.696923425058676,0.804737854124365,
0.696923425058676,0.804737854124365,0.696923425058676,0.804737854124365,
0.696923425058676,0.804737854124365,0.696923425058676,0.804737854124365,
0.696923425058676,0.804737854124365,0.696923425058676,0.804737854124365,
0.696923425058676,0.804737854124365,0.696923425058676,0.804737854124365,
0.696923425058676,0.804737854124365,0.696923425058676,0.804737854124365,
0.696923425058676,0.804737854124365,0.696923425058676,0.804737854124365,
0.696923425058676,0.804737854124365,0.696923425058676,0.804737854124365,
0.696923425058676,0.804737854124365,0.696923425058676,0.804737854124365,
0.696923425058676,0.804737854124365,0.696923425058676,0.804737854124365,
0.696923425058676,0.804737854124365,0.696923425058676,0.804737854124365,
0.696923425058676,0.804737854124365,0.696923425058676,0.804737854124365,
0.696923425058676,0.804737854124365,0.696923425058676,0.804737854124365,
0.696923425058676,0.804737854124365,0.696923425058676,0.804737854124365),
(1.,0.866025403784439,1.,0.866025403784439,1.,0.866025403784439,1.,0.866025403784439,
1.,0.866025403784439,1.,0.866025403784439,1.,0.866025403784439,1.,0.866025403784439,
1.,0.866025403784439,1.,0.866025403784439,1.,0.866025403784439,1.,0.866025403784439,
1.,0.866025403784439,1.,0.866025403784439,1.,0.866025403784439,1.,0.866025403784439,
1.,0.866025403784439,1.,0.866025403784439,1.,0.866025403784439,1.,0.866025403784439,
1.,0.866025403784439,1.,0.866025403784439,1.,0.866025403784439,1.,0.866025403784439,
1.,0.866025403784439,1.,0.866025403784439,1.,0.866025403784439,1.,0.866025403784439,
1.,0.866025403784439,1.,0.866025403784439,1.,0.866025403784439,1.,0.866025403784439,
1.,0.866025403784439,1.,0.866025403784439,1.,0.866025403784439,1.,0.866025403784439,
1.)))
REPRESENTATION_ITEM('')
SURFACE()
);
#438=(
BOUNDED_SURFACE()
B_SPLINE_SURFACE(3,2,((#20778,#20779,#20780,#20781,#20782,#20783,#20784,
#20785,#20786,#20787,#20788,#20789,#20790,#20791,#20792,#20793,#20794,#20795,
#20796,#20797,#20798,#20799,#20800,#20801,#20802,#20803,#20804,#20805,#20806,
#20807,#20808,#20809,#20810,#20811,#20812,#20813,#20814,#20815,#20816,#20817,
#20818,#20819,#20820,#20821,#20822,#20823,#20824,#20825,#20826,#20827,#20828,
#20829,#20830,#20831,#20832,#20833,#20834,#20835,#20836,#20837,#20838,#20839,
#20840,#20841,#20842,#20843,#20844,#20845,#20846,#20847,#20848,#20849,#20850),
(#20851,#20852,#20853,#20854,#20855,#20856,#20857,#20858,#20859,#20860,
#20861,#20862,#20863,#20864,#20865,#20866,#20867,#20868,#20869,#20870,#20871,
#20872,#20873,#20874,#20875,#20876,#20877,#20878,#20879,#20880,#20881,#20882,
#20883,#20884,#20885,#20886,#20887,#20888,#20889,#20890,#20891,#20892,#20893,
#20894,#20895,#20896,#20897,#20898,#20899,#20900,#20901,#20902,#20903,#20904,
#20905,#20906,#20907,#20908,#20909,#20910,#20911,#20912,#20913,#20914,#20915,
#20916,#20917,#20918,#20919,#20920,#20921,#20922,#20923),(#20924,#20925,
#20926,#20927,#20928,#20929,#20930,#20931,#20932,#20933,#20934,#20935,#20936,
#20937,#20938,#20939,#20940,#20941,#20942,#20943,#20944,#20945,#20946,#20947,
#20948,#20949,#20950,#20951,#20952,#20953,#20954,#20955,#20956,#20957,#20958,
#20959,#20960,#20961,#20962,#20963,#20964,#20965,#20966,#20967,#20968,#20969,
#20970,#20971,#20972,#20973,#20974,#20975,#20976,#20977,#20978,#20979,#20980,
#20981,#20982,#20983,#20984,#20985,#20986,#20987,#20988,#20989,#20990,#20991,
#20992,#20993,#20994,#20995,#20996),(#20997,#20998,#20999,#21000,#21001,
#21002,#21003,#21004,#21005,#21006,#21007,#21008,#21009,#21010,#21011,#21012,
#21013,#21014,#21015,#21016,#21017,#21018,#21019,#21020,#21021,#21022,#21023,
#21024,#21025,#21026,#21027,#21028,#21029,#21030,#21031,#21032,#21033,#21034,
#21035,#21036,#21037,#21038,#21039,#21040,#21041,#21042,#21043,#21044,#21045,
#21046,#21047,#21048,#21049,#21050,#21051,#21052,#21053,#21054,#21055,#21056,
#21057,#21058,#21059,#21060,#21061,#21062,#21063,#21064,#21065,#21066,#21067,
#21068,#21069)),.UNSPECIFIED.,.F.,.F.,.F.)
B_SPLINE_SURFACE_WITH_KNOTS((4,4),(3,2,2,2,2,2,2,2,2,2,2,2,2,2,2,2,2,2,
2,2,2,2,2,2,2,2,2,2,2,2,2,2,2,2,2,2,3),(0.,1.),(0.,0.0277777777777778,0.0555555555555556,
0.0833333333333333,0.111111111111111,0.138888888888889,0.166666666666667,
0.194444444444444,0.222222222222222,0.25,0.277777777777778,0.305555555555556,
0.333333333333333,0.361111111111111,0.388888888888889,0.416666666666667,
0.444444444444444,0.472222222222222,0.5,0.527777777777778,0.555555555555556,
0.583333333333333,0.611111111111111,0.638888888888889,0.666666666666667,
0.694444444444444,0.722222222222222,0.75,0.777777777777778,0.805555555555556,
0.833333333333333,0.861111111111111,0.888888888888889,0.916666666666667,
0.944444444444444,0.972222222222222,1.),.UNSPECIFIED.)
GEOMETRIC_REPRESENTATION_ITEM()
RATIONAL_B_SPLINE_SURFACE(((1.,0.866025403784439,1.,0.866025403784439,1.,
0.866025403784439,1.,0.866025403784439,1.,0.866025403784439,1.,0.866025403784439,
1.,0.866025403784439,1.,0.866025403784439,1.,0.866025403784439,1.,0.866025403784439,
1.,0.866025403784439,1.,0.866025403784439,1.,0.866025403784439,1.,0.866025403784439,
1.,0.866025403784439,1.,0.866025403784439,1.,0.866025403784439,1.,0.866025403784439,
1.,0.866025403784439,1.,0.866025403784439,1.,0.866025403784439,1.,0.866025403784439,
1.,0.866025403784439,1.,0.866025403784439,1.,0.866025403784439,1.,0.866025403784439,
1.,0.866025403784439,1.,0.866025403784439,1.,0.866025403784439,1.,0.866025403784439,
1.,0.866025403784439,1.,0.866025403784439,1.,0.866025403784439,1.,0.866025403784439,
1.,0.866025403784439,1.,0.866025403784439,1.),(0.804737854124365,0.696923425058676,
0.804737854124365,0.696923425058676,0.804737854124365,0.696923425058676,
0.804737854124365,0.696923425058676,0.804737854124365,0.696923425058676,
0.804737854124365,0.696923425058676,0.804737854124365,0.696923425058676,
0.804737854124365,0.696923425058676,0.804737854124365,0.696923425058676,
0.804737854124365,0.696923425058676,0.804737854124365,0.696923425058676,
0.804737854124365,0.696923425058676,0.804737854124365,0.696923425058676,
0.804737854124365,0.696923425058676,0.804737854124365,0.696923425058676,
0.804737854124365,0.696923425058676,0.804737854124365,0.696923425058676,
0.804737854124365,0.696923425058676,0.804737854124365,0.696923425058676,
0.804737854124365,0.696923425058676,0.804737854124365,0.696923425058676,
0.804737854124365,0.696923425058676,0.804737854124365,0.696923425058676,
0.804737854124365,0.696923425058676,0.804737854124365,0.696923425058676,
0.804737854124365,0.696923425058676,0.804737854124365,0.696923425058676,
0.804737854124365,0.696923425058676,0.804737854124365,0.696923425058676,
0.804737854124365,0.696923425058676,0.804737854124365,0.696923425058676,
0.804737854124365,0.696923425058676,0.804737854124365,0.696923425058676,
0.804737854124365,0.696923425058676,0.804737854124365,0.696923425058676,
0.804737854124365,0.696923425058676,0.804737854124365),(0.804737854124365,
0.696923425058676,0.804737854124365,0.696923425058676,0.804737854124365,
0.696923425058676,0.804737854124365,0.696923425058676,0.804737854124365,
0.696923425058676,0.804737854124365,0.696923425058676,0.804737854124365,
0.696923425058676,0.804737854124365,0.696923425058676,0.804737854124365,
0.696923425058676,0.804737854124365,0.696923425058676,0.804737854124365,
0.696923425058676,0.804737854124365,0.696923425058676,0.804737854124365,
0.696923425058676,0.804737854124365,0.696923425058676,0.804737854124365,
0.696923425058676,0.804737854124365,0.696923425058676,0.804737854124365,
0.696923425058676,0.804737854124365,0.696923425058676,0.804737854124365,
0.696923425058676,0.804737854124365,0.696923425058676,0.804737854124365,
0.696923425058676,0.804737854124365,0.696923425058676,0.804737854124365,
0.696923425058676,0.804737854124365,0.696923425058676,0.804737854124365,
0.696923425058676,0.804737854124365,0.696923425058676,0.804737854124365,
0.696923425058676,0.804737854124365,0.696923425058676,0.804737854124365,
0.696923425058676,0.804737854124365,0.696923425058676,0.804737854124365,
0.696923425058676,0.804737854124365,0.696923425058676,0.804737854124365,
0.696923425058676,0.804737854124365,0.696923425058676,0.804737854124365,
0.696923425058676,0.804737854124365,0.696923425058676,0.804737854124365),
(1.,0.866025403784439,1.,0.866025403784439,1.,0.866025403784439,1.,0.866025403784439,
1.,0.866025403784439,1.,0.866025403784439,1.,0.866025403784439,1.,0.866025403784439,
1.,0.866025403784439,1.,0.866025403784439,1.,0.866025403784439,1.,0.866025403784439,
1.,0.866025403784439,1.,0.866025403784439,1.,0.866025403784439,1.,0.866025403784439,
1.,0.866025403784439,1.,0.866025403784439,1.,0.866025403784439,1.,0.866025403784439,
1.,0.866025403784439,1.,0.866025403784439,1.,0.866025403784439,1.,0.866025403784439,
1.,0.866025403784439,1.,0.866025403784439,1.,0.866025403784439,1.,0.866025403784439,
1.,0.866025403784439,1.,0.866025403784439,1.,0.866025403784439,1.,0.866025403784439,
1.,0.866025403784439,1.,0.866025403784439,1.,0.866025403784439,1.,0.866025403784439,
1.)))
REPRESENTATION_ITEM('')
SURFACE()
);
#896=PLANE('',#10686);
#897=PLANE('',#10687);
#1262=FACE_OUTER_BOUND('',#1840,.T.);
#1263=FACE_OUTER_BOUND('',#1841,.T.);
#1264=FACE_OUTER_BOUND('',#1842,.T.);
#1265=FACE_OUTER_BOUND('',#1843,.T.);
#1266=FACE_OUTER_BOUND('',#1844,.T.);
#1267=FACE_OUTER_BOUND('',#1845,.T.);
#1840=EDGE_LOOP('',(#7694,#7695,#7696,#7697,#7698));
#1841=EDGE_LOOP('',(#7699,#7700,#7701,#7702,#7703));
#1842=EDGE_LOOP('',(#7704,#7705,#7706,#7707,#7708));
#1843=EDGE_LOOP('',(#7709,#7710,#7711,#7712,#7713));
#1844=EDGE_LOOP('',(#7714,#7715,#7716,#7717));
#1845=EDGE_LOOP('',(#7718,#7719,#7720,#7721));
#2387=CIRCLE('',#10678,0.35);
#2388=CIRCLE('',#10679,0.35);
#2389=CIRCLE('',#10680,0.35);
#2390=CIRCLE('',#10681,0.35);
#2391=CIRCLE('',#10682,0.35);
#2392=CIRCLE('',#10683,0.35);
#2393=CIRCLE('',#10684,0.35);
#2394=CIRCLE('',#10685,0.35);
#4515=VERTEX_POINT('',#19886);
#4516=VERTEX_POINT('',#19887);
#4517=VERTEX_POINT('',#19889);
#4518=VERTEX_POINT('',#19903);
#4519=VERTEX_POINT('',#19965);
#4520=VERTEX_POINT('',#20332);
#4521=VERTEX_POINT('',#20701);
#4522=VERTEX_POINT('',#20703);
#5660=EDGE_CURVE('',#4515,#4516,#2387,.T.);
#5661=EDGE_CURVE('',#4517,#4516,#196,.T.);
#5662=EDGE_CURVE('',#4518,#4517,#197,.T.);
#5663=EDGE_CURVE('',#4519,#4518,#2388,.T.);
#5664=EDGE_CURVE('',#4519,#4515,#198,.T.);
#5665=EDGE_CURVE('',#4520,#4519,#2389,.T.);
#5666=EDGE_CURVE('',#4520,#4518,#199,.T.);
#5667=EDGE_CURVE('',#4518,#4517,#200,.T.);
#5668=EDGE_CURVE('',#4517,#4515,#2390,.T.);
#5669=EDGE_CURVE('',#4521,#4520,#2391,.T.);
#5670=EDGE_CURVE('',#4521,#4522,#201,.T.);
#5671=EDGE_CURVE('',#4522,#4517,#2392,.T.);
#5672=EDGE_CURVE('',#4518,#4521,#2393,.T.);
#5673=EDGE_CURVE('',#4516,#4522,#2394,.T.);
#7694=ORIENTED_EDGE('',*,*,#5660,.T.);
#7695=ORIENTED_EDGE('',*,*,#5661,.F.);
#7696=ORIENTED_EDGE('',*,*,#5662,.F.);
#7697=ORIENTED_EDGE('',*,*,#5663,.F.);
#7698=ORIENTED_EDGE('',*,*,#5664,.T.);
#7699=ORIENTED_EDGE('',*,*,#5664,.F.);
#7700=ORIENTED_EDGE('',*,*,#5665,.F.);
#7701=ORIENTED_EDGE('',*,*,#5666,.T.);
#7702=ORIENTED_EDGE('',*,*,#5667,.T.);
#7703=ORIENTED_EDGE('',*,*,#5668,.T.);
#7704=ORIENTED_EDGE('',*,*,#5666,.F.);
#7705=ORIENTED_EDGE('',*,*,#5669,.F.);
#7706=ORIENTED_EDGE('',*,*,#5670,.T.);
#7707=ORIENTED_EDGE('',*,*,#5671,.T.);
#7708=ORIENTED_EDGE('',*,*,#5667,.F.);
#7709=ORIENTED_EDGE('',*,*,#5670,.F.);
#7710=ORIENTED_EDGE('',*,*,#5672,.F.);
#7711=ORIENTED_EDGE('',*,*,#5662,.T.);
#7712=ORIENTED_EDGE('',*,*,#5661,.T.);
#7713=ORIENTED_EDGE('',*,*,#5673,.T.);
#7714=ORIENTED_EDGE('',*,*,#5673,.F.);
#7715=ORIENTED_EDGE('',*,*,#5660,.F.);
#7716=ORIENTED_EDGE('',*,*,#5668,.F.);
#7717=ORIENTED_EDGE('',*,*,#5671,.F.);
#7718=ORIENTED_EDGE('',*,*,#5672,.T.);
#7719=ORIENTED_EDGE('',*,*,#5669,.T.);
#7720=ORIENTED_EDGE('',*,*,#5665,.T.);
#7721=ORIENTED_EDGE('',*,*,#5663,.T.);
#9628=ADVANCED_FACE('',(#1262),#435,.F.);
#9629=ADVANCED_FACE('',(#1263),#436,.F.);
#9630=ADVANCED_FACE('',(#1264),#437,.F.);
#9631=ADVANCED_FACE('',(#1265),#438,.F.);
#9632=ADVANCED_FACE('',(#1266),#896,.F.);
#9633=ADVANCED_FACE('',(#1267),#897,.T.);
#9948=CLOSED_SHELL('',(#9628,#9629,#9630,#9631,#9632,#9633));
#10677=AXIS2_PLACEMENT_3D('',#19593,#12467,#12468);
#10678=AXIS2_PLACEMENT_3D('',#19888,#12469,#12470);
#10679=AXIS2_PLACEMENT_3D('',#19966,#12471,#12472);
#10680=AXIS2_PLACEMENT_3D('',#20333,#12473,#12474);
#10681=AXIS2_PLACEMENT_3D('',#20408,#12475,#12476);
#10682=AXIS2_PLACEMENT_3D('',#20702,#12477,#12478);
#10683=AXIS2_PLACEMENT_3D('',#20777,#12479,#12480);
#10684=AXIS2_PLACEMENT_3D('',#21070,#12481,#12482);
#10685=AXIS2_PLACEMENT_3D('',#21071,#12483,#12484);
#10686=AXIS2_PLACEMENT_3D('',#21072,#12485,#12486);
#10687=AXIS2_PLACEMENT_3D('',#21073,#12487,#12488);
#12467=DIRECTION('axis',(0.,0.,1.));
#12468=DIRECTION('refdir',(1.,0.,0.));
#12469=DIRECTION('center_axis',(1.,0.,8.37955521322352E-14));
#12470=DIRECTION('ref_axis',(8.37955521322352E-14,0.,-1.));
#12471=DIRECTION('center_axis',(1.,0.,0.));
#12472=DIRECTION('ref_axis',(0.,0.,-1.));
#12473=DIRECTION('center_axis',(1.,0.,0.));
#12474=DIRECTION('ref_axis',(0.,0.,-1.));
#12475=DIRECTION('center_axis',(1.,0.,8.37955521322352E-14));
#12476=DIRECTION('ref_axis',(8.37955521322352E-14,0.,-1.));
#12477=DIRECTION('center_axis',(1.,0.,0.));
#12478=DIRECTION('ref_axis',(0.,0.,-1.));
#12479=DIRECTION('center_axis',(1.,0.,8.37955521322352E-14));
#12480=DIRECTION('ref_axis',(8.37955521322352E-14,0.,-1.));
#12481=DIRECTION('center_axis',(1.,0.,0.));
#12482=DIRECTION('ref_axis',(0.,0.,-1.));
#12483=DIRECTION('center_axis',(1.,0.,8.37955521322352E-14));
#12484=DIRECTION('ref_axis',(8.37955521322352E-14,0.,-1.));
#12485=DIRECTION('center_axis',(1.,0.,8.37955521322352E-14));
#12486=DIRECTION('ref_axis',(8.37955521322352E-14,0.,-1.));
#12487=DIRECTION('center_axis',(1.,0.,0.));
#12488=DIRECTION('ref_axis',(0.,0.,-1.));
#19593=CARTESIAN_POINT('',(0.,0.,0.));
#19594=CARTESIAN_POINT('Ctrl Pts',(0.,0.,1.8));
#19595=CARTESIAN_POINT('Ctrl Pts',(-1.03923048454133,0.0583333333333332,
1.8));
#19596=CARTESIAN_POINT('Ctrl Pts',(-1.55884572681199,0.116666666666666,
0.9));
#19597=CARTESIAN_POINT('Ctrl Pts',(-2.07846096908265,0.175,1.27269028646989E-16));
#19598=CARTESIAN_POINT('Ctrl Pts',(-1.55884572681199,0.233333333333333,
-0.9));
#19599=CARTESIAN_POINT('Ctrl Pts',(-1.03923048454133,0.291666666666666,
-1.8));
#19600=CARTESIAN_POINT('Ctrl Pts',(-2.20436423846524E-16,0.349999999999999,
-1.8));
#19601=CARTESIAN_POINT('Ctrl Pts',(1.03923048454133,0.408333333333333,-1.8));
#19602=CARTESIAN_POINT('Ctrl Pts',(1.55884572681199,0.466666666666666,-0.900000000000001));
#19603=CARTESIAN_POINT('Ctrl Pts',(2.07846096908265,0.524999999999999,-3.81807085940967E-16));
#19604=CARTESIAN_POINT('Ctrl Pts',(1.55884572681199,0.583333333333332,0.899999999999999));
#19605=CARTESIAN_POINT('Ctrl Pts',(1.03923048454133,0.641666666666665,1.8));
#19606=CARTESIAN_POINT('Ctrl Pts',(0.,0.699999999999999,1.8));
#19607=CARTESIAN_POINT('Ctrl Pts',(-1.03923048454133,0.758333333333332,
1.8));
#19608=CARTESIAN_POINT('Ctrl Pts',(-1.55884572681199,0.816666666666665,
0.9));
#19609=CARTESIAN_POINT('Ctrl Pts',(-2.07846096908265,0.874999999999998,
1.27269028646989E-16));
#19610=CARTESIAN_POINT('Ctrl Pts',(-1.55884572681199,0.933333333333332,
-0.9));
#19611=CARTESIAN_POINT('Ctrl Pts',(-1.03923048454133,0.991666666666665,
-1.8));
#19612=CARTESIAN_POINT('Ctrl Pts',(-2.20436423846524E-16,1.05,-1.8));
#19613=CARTESIAN_POINT('Ctrl Pts',(1.03923048454133,1.10833333333333,-1.8));
#19614=CARTESIAN_POINT('Ctrl Pts',(1.55884572681199,1.16666666666666,-0.900000000000001));
#19615=CARTESIAN_POINT('Ctrl Pts',(2.07846096908265,1.225,-3.81807085940967E-16));
#19616=CARTESIAN_POINT('Ctrl Pts',(1.55884572681199,1.28333333333333,0.899999999999999));
#19617=CARTESIAN_POINT('Ctrl Pts',(1.03923048454133,1.34166666666666,1.8));
#19618=CARTESIAN_POINT('Ctrl Pts',(0.,1.4,1.8));
#19619=CARTESIAN_POINT('Ctrl Pts',(-1.03923048454133,1.45833333333333,1.8));
#19620=CARTESIAN_POINT('Ctrl Pts',(-1.55884572681199,1.51666666666666,0.9));
#19621=CARTESIAN_POINT('Ctrl Pts',(-2.07846096908265,1.575,1.27269028646989E-16));
#19622=CARTESIAN_POINT('Ctrl Pts',(-1.55884572681199,1.63333333333333,-0.9));
#19623=CARTESIAN_POINT('Ctrl Pts',(-1.03923048454133,1.69166666666666,-1.8));
#19624=CARTESIAN_POINT('Ctrl Pts',(-2.20436423846524E-16,1.75,-1.8));
#19625=CARTESIAN_POINT('Ctrl Pts',(1.03923048454133,1.80833333333333,-1.8));
#19626=CARTESIAN_POINT('Ctrl Pts',(1.55884572681199,1.86666666666666,-0.900000000000001));
#19627=CARTESIAN_POINT('Ctrl Pts',(2.07846096908265,1.925,-3.81807085940967E-16));
#19628=CARTESIAN_POINT('Ctrl Pts',(1.55884572681199,1.98333333333333,0.899999999999999));
#19629=CARTESIAN_POINT('Ctrl Pts',(1.03923048454133,2.04166666666666,1.8));
#19630=CARTESIAN_POINT('Ctrl Pts',(0.,2.1,1.8));
#19631=CARTESIAN_POINT('Ctrl Pts',(-1.03923048454133,2.15833333333333,1.8));
#19632=CARTESIAN_POINT('Ctrl Pts',(-1.55884572681199,2.21666666666666,0.9));
#19633=CARTESIAN_POINT('Ctrl Pts',(-2.07846096908265,2.275,1.27269028646989E-16));
#19634=CARTESIAN_POINT('Ctrl Pts',(-1.55884572681199,2.33333333333333,-0.9));
#19635=CARTESIAN_POINT('Ctrl Pts',(-1.03923048454133,2.39166666666666,-1.8));
#19636=CARTESIAN_POINT('Ctrl Pts',(-2.20436423846524E-16,2.45,-1.8));
#19637=CARTESIAN_POINT('Ctrl Pts',(1.03923048454133,2.50833333333333,-1.8));
#19638=CARTESIAN_POINT('Ctrl Pts',(1.55884572681199,2.56666666666666,-0.900000000000001));
#19639=CARTESIAN_POINT('Ctrl Pts',(2.07846096908265,2.62499999999999,-3.81807085940967E-16));
#19640=CARTESIAN_POINT('Ctrl Pts',(1.55884572681199,2.68333333333333,0.899999999999999));
#19641=CARTESIAN_POINT('Ctrl Pts',(1.03923048454133,2.74166666666666,1.8));
#19642=CARTESIAN_POINT('Ctrl Pts',(0.,2.79999999999999,1.8));
#19643=CARTESIAN_POINT('Ctrl Pts',(-1.03923048454133,2.85833333333333,1.8));
#19644=CARTESIAN_POINT('Ctrl Pts',(-1.55884572681199,2.91666666666666,0.9));
#19645=CARTESIAN_POINT('Ctrl Pts',(-2.07846096908265,2.97499999999999,1.27269028646989E-16));
#19646=CARTESIAN_POINT('Ctrl Pts',(-1.55884572681199,3.03333333333333,-0.9));
#19647=CARTESIAN_POINT('Ctrl Pts',(-1.03923048454133,3.09166666666666,-1.8));
#19648=CARTESIAN_POINT('Ctrl Pts',(-2.20436423846524E-16,3.14999999999999,
-1.8));
#19649=CARTESIAN_POINT('Ctrl Pts',(1.03923048454133,3.20833333333333,-1.8));
#19650=CARTESIAN_POINT('Ctrl Pts',(1.55884572681199,3.26666666666666,-0.900000000000001));
#19651=CARTESIAN_POINT('Ctrl Pts',(2.07846096908265,3.32499999999999,-3.81807085940967E-16));
#19652=CARTESIAN_POINT('Ctrl Pts',(1.55884572681199,3.38333333333333,0.899999999999999));
#19653=CARTESIAN_POINT('Ctrl Pts',(1.03923048454133,3.44166666666666,1.8));
#19654=CARTESIAN_POINT('Ctrl Pts',(0.,3.49999999999999,1.8));
#19655=CARTESIAN_POINT('Ctrl Pts',(-1.03923048454133,3.55833333333333,1.8));
#19656=CARTESIAN_POINT('Ctrl Pts',(-1.55884572681199,3.61666666666666,0.9));
#19657=CARTESIAN_POINT('Ctrl Pts',(-2.07846096908265,3.67499999999999,1.27269028646989E-16));
#19658=CARTESIAN_POINT('Ctrl Pts',(-1.55884572681199,3.73333333333333,-0.9));
#19659=CARTESIAN_POINT('Ctrl Pts',(-1.03923048454133,3.79166666666666,-1.8));
#19660=CARTESIAN_POINT('Ctrl Pts',(-2.20436423846524E-16,3.84999999999999,
-1.8));
#19661=CARTESIAN_POINT('Ctrl Pts',(1.03923048454133,3.90833333333333,-1.8));
#19662=CARTESIAN_POINT('Ctrl Pts',(1.55884572681199,3.96666666666666,-0.900000000000001));
#19663=CARTESIAN_POINT('Ctrl Pts',(2.07846096908265,4.02499999999999,-3.81807085940967E-16));
#19664=CARTESIAN_POINT('Ctrl Pts',(1.55884572681199,4.08333333333333,0.899999999999999));
#19665=CARTESIAN_POINT('Ctrl Pts',(1.03923048454133,4.14166666666666,1.8));
#19666=CARTESIAN_POINT('Ctrl Pts',(0.,4.19999999999999,1.8));
#19667=CARTESIAN_POINT('Ctrl Pts',(0.,0.205025253169417,1.8));
#19668=CARTESIAN_POINT('Ctrl Pts',(-1.03923048454133,0.26335858650275,1.8));
#19669=CARTESIAN_POINT('Ctrl Pts',(-1.55884572681199,0.321691919836083,
0.9));
#19670=CARTESIAN_POINT('Ctrl Pts',(-2.07846096908265,0.380025253169416,
1.27269028646989E-16));
#19671=CARTESIAN_POINT('Ctrl Pts',(-1.55884572681199,0.43835858650275,-0.9));
#19672=CARTESIAN_POINT('Ctrl Pts',(-1.03923048454133,0.496691919836083,
-1.8));
#19673=CARTESIAN_POINT('Ctrl Pts',(-2.20436423846524E-16,0.555025253169416,
-1.8));
#19674=CARTESIAN_POINT('Ctrl Pts',(1.03923048454133,0.613358586502749,-1.8));
#19675=CARTESIAN_POINT('Ctrl Pts',(1.55884572681199,0.671691919836083,-0.900000000000001));
#19676=CARTESIAN_POINT('Ctrl Pts',(2.07846096908265,0.730025253169416,-3.81807085940967E-16));
#19677=CARTESIAN_POINT('Ctrl Pts',(1.55884572681199,0.788358586502749,0.899999999999999));
#19678=CARTESIAN_POINT('Ctrl Pts',(1.03923048454133,0.846691919836082,1.8));
#19679=CARTESIAN_POINT('Ctrl Pts',(0.,0.905025253169415,1.8));
#19680=CARTESIAN_POINT('Ctrl Pts',(-1.03923048454133,0.963358586502749,
1.8));
#19681=CARTESIAN_POINT('Ctrl Pts',(-1.55884572681199,1.02169191983608,0.9));
#19682=CARTESIAN_POINT('Ctrl Pts',(-2.07846096908265,1.08002525316942,1.27269028646989E-16));
#19683=CARTESIAN_POINT('Ctrl Pts',(-1.55884572681199,1.13835858650275,-0.9));
#19684=CARTESIAN_POINT('Ctrl Pts',(-1.03923048454133,1.19669191983608,-1.8));
#19685=CARTESIAN_POINT('Ctrl Pts',(-2.20436423846524E-16,1.25502525316941,
-1.8));
#19686=CARTESIAN_POINT('Ctrl Pts',(1.03923048454133,1.31335858650275,-1.8));
#19687=CARTESIAN_POINT('Ctrl Pts',(1.55884572681199,1.37169191983608,-0.900000000000001));
#19688=CARTESIAN_POINT('Ctrl Pts',(2.07846096908265,1.43002525316941,-3.81807085940967E-16));
#19689=CARTESIAN_POINT('Ctrl Pts',(1.55884572681199,1.48835858650275,0.899999999999999));
#19690=CARTESIAN_POINT('Ctrl Pts',(1.03923048454133,1.54669191983608,1.8));
#19691=CARTESIAN_POINT('Ctrl Pts',(0.,1.60502525316941,1.8));
#19692=CARTESIAN_POINT('Ctrl Pts',(-1.03923048454133,1.66335858650275,1.8));
#19693=CARTESIAN_POINT('Ctrl Pts',(-1.55884572681199,1.72169191983608,0.9));
#19694=CARTESIAN_POINT('Ctrl Pts',(-2.07846096908265,1.78002525316941,1.27269028646989E-16));
#19695=CARTESIAN_POINT('Ctrl Pts',(-1.55884572681199,1.83835858650275,-0.9));
#19696=CARTESIAN_POINT('Ctrl Pts',(-1.03923048454133,1.89669191983608,-1.8));
#19697=CARTESIAN_POINT('Ctrl Pts',(-2.20436423846524E-16,1.95502525316941,
-1.8));
#19698=CARTESIAN_POINT('Ctrl Pts',(1.03923048454133,2.01335858650275,-1.8));
#19699=CARTESIAN_POINT('Ctrl Pts',(1.55884572681199,2.07169191983608,-0.900000000000001));
#19700=CARTESIAN_POINT('Ctrl Pts',(2.07846096908265,2.13002525316941,-3.81807085940967E-16));
#19701=CARTESIAN_POINT('Ctrl Pts',(1.55884572681199,2.18835858650275,0.899999999999999));
#19702=CARTESIAN_POINT('Ctrl Pts',(1.03923048454133,2.24669191983608,1.8));
#19703=CARTESIAN_POINT('Ctrl Pts',(0.,2.30502525316941,1.8));
#19704=CARTESIAN_POINT('Ctrl Pts',(-1.03923048454133,2.36335858650275,1.8));
#19705=CARTESIAN_POINT('Ctrl Pts',(-1.55884572681199,2.42169191983608,0.9));
#19706=CARTESIAN_POINT('Ctrl Pts',(-2.07846096908265,2.48002525316941,1.27269028646989E-16));
#19707=CARTESIAN_POINT('Ctrl Pts',(-1.55884572681199,2.53835858650275,-0.9));
#19708=CARTESIAN_POINT('Ctrl Pts',(-1.03923048454133,2.59669191983608,-1.8));
#19709=CARTESIAN_POINT('Ctrl Pts',(-2.20436423846524E-16,2.65502525316941,
-1.8));
#19710=CARTESIAN_POINT('Ctrl Pts',(1.03923048454133,2.71335858650274,-1.8));
#19711=CARTESIAN_POINT('Ctrl Pts',(1.55884572681199,2.77169191983608,-0.900000000000001));
#19712=CARTESIAN_POINT('Ctrl Pts',(2.07846096908265,2.83002525316941,-3.81807085940967E-16));
#19713=CARTESIAN_POINT('Ctrl Pts',(1.55884572681199,2.88835858650274,0.899999999999999));
#19714=CARTESIAN_POINT('Ctrl Pts',(1.03923048454133,2.94669191983608,1.8));
#19715=CARTESIAN_POINT('Ctrl Pts',(0.,3.00502525316941,1.8));
#19716=CARTESIAN_POINT('Ctrl Pts',(-1.03923048454133,3.06335858650274,1.8));
#19717=CARTESIAN_POINT('Ctrl Pts',(-1.55884572681199,3.12169191983608,0.9));
#19718=CARTESIAN_POINT('Ctrl Pts',(-2.07846096908265,3.18002525316941,1.27269028646989E-16));
#19719=CARTESIAN_POINT('Ctrl Pts',(-1.55884572681199,3.23835858650274,-0.9));
#19720=CARTESIAN_POINT('Ctrl Pts',(-1.03923048454133,3.29669191983608,-1.8));
#19721=CARTESIAN_POINT('Ctrl Pts',(-2.20436423846524E-16,3.35502525316941,
-1.8));
#19722=CARTESIAN_POINT('Ctrl Pts',(1.03923048454133,3.41335858650274,-1.8));
#19723=CARTESIAN_POINT('Ctrl Pts',(1.55884572681199,3.47169191983608,-0.900000000000001));
#19724=CARTESIAN_POINT('Ctrl Pts',(2.07846096908265,3.53002525316941,-3.81807085940967E-16));
#19725=CARTESIAN_POINT('Ctrl Pts',(1.55884572681199,3.58835858650274,0.899999999999999));
#19726=CARTESIAN_POINT('Ctrl Pts',(1.03923048454133,3.64669191983608,1.8));
#19727=CARTESIAN_POINT('Ctrl Pts',(0.,3.70502525316941,1.8));
#19728=CARTESIAN_POINT('Ctrl Pts',(-1.03923048454133,3.76335858650274,1.8));
#19729=CARTESIAN_POINT('Ctrl Pts',(-1.55884572681199,3.82169191983608,0.9));
#19730=CARTESIAN_POINT('Ctrl Pts',(-2.07846096908265,3.88002525316941,1.27269028646989E-16));
#19731=CARTESIAN_POINT('Ctrl Pts',(-1.55884572681199,3.93835858650274,-0.9));
#19732=CARTESIAN_POINT('Ctrl Pts',(-1.03923048454133,3.99669191983608,-1.8));
#19733=CARTESIAN_POINT('Ctrl Pts',(-2.20436423846524E-16,4.05502525316941,
-1.8));
#19734=CARTESIAN_POINT('Ctrl Pts',(1.03923048454133,4.11335858650274,-1.8));
#19735=CARTESIAN_POINT('Ctrl Pts',(1.55884572681199,4.17169191983608,-0.900000000000001));
#19736=CARTESIAN_POINT('Ctrl Pts',(2.07846096908265,4.23002525316941,-3.81807085940967E-16));
#19737=CARTESIAN_POINT('Ctrl Pts',(1.55884572681199,4.28835858650274,0.899999999999999));
#19738=CARTESIAN_POINT('Ctrl Pts',(1.03923048454133,4.34669191983608,1.8));
#19739=CARTESIAN_POINT('Ctrl Pts',(0.,4.40502525316941,1.8));
#19740=CARTESIAN_POINT('Ctrl Pts',(0.,0.35,1.94497474683058));
#19741=CARTESIAN_POINT('Ctrl Pts',(-1.12293169364966,0.408333333333333,
1.94497474683058));
#19742=CARTESIAN_POINT('Ctrl Pts',(-1.68439754047449,0.466666666666666,
0.972487373415292));
#19743=CARTESIAN_POINT('Ctrl Pts',(-2.24586338729932,0.525,1.37519470428917E-16));
#19744=CARTESIAN_POINT('Ctrl Pts',(-1.68439754047449,0.583333333333333,
-0.972487373415291));
#19745=CARTESIAN_POINT('Ctrl Pts',(-1.12293169364966,0.641666666666666,
-1.94497474683058));
#19746=CARTESIAN_POINT('Ctrl Pts',(-2.38190709812851E-16,0.699999999999999,
-1.94497474683058));
#19747=CARTESIAN_POINT('Ctrl Pts',(1.12293169364966,0.758333333333333,-1.94497474683058));
#19748=CARTESIAN_POINT('Ctrl Pts',(1.68439754047449,0.816666666666666,-0.972487373415292));
#19749=CARTESIAN_POINT('Ctrl Pts',(2.24586338729932,0.874999999999999,-4.12558411286752E-16));
#19750=CARTESIAN_POINT('Ctrl Pts',(1.68439754047449,0.933333333333332,0.97248737341529));
#19751=CARTESIAN_POINT('Ctrl Pts',(1.12293169364966,0.991666666666665,1.94497474683058));
#19752=CARTESIAN_POINT('Ctrl Pts',(0.,1.05,1.94497474683058));
#19753=CARTESIAN_POINT('Ctrl Pts',(-1.12293169364966,1.10833333333333,1.94497474683058));
#19754=CARTESIAN_POINT('Ctrl Pts',(-1.68439754047449,1.16666666666666,0.972487373415292));
#19755=CARTESIAN_POINT('Ctrl Pts',(-2.24586338729932,1.225,1.37519470428917E-16));
#19756=CARTESIAN_POINT('Ctrl Pts',(-1.68439754047449,1.28333333333333,-0.972487373415291));
#19757=CARTESIAN_POINT('Ctrl Pts',(-1.12293169364966,1.34166666666667,-1.94497474683058));
#19758=CARTESIAN_POINT('Ctrl Pts',(-2.38190709812851E-16,1.4,-1.94497474683058));
#19759=CARTESIAN_POINT('Ctrl Pts',(1.12293169364966,1.45833333333333,-1.94497474683058));
#19760=CARTESIAN_POINT('Ctrl Pts',(1.68439754047449,1.51666666666666,-0.972487373415292));
#19761=CARTESIAN_POINT('Ctrl Pts',(2.24586338729932,1.575,-4.12558411286752E-16));
#19762=CARTESIAN_POINT('Ctrl Pts',(1.68439754047449,1.63333333333333,0.97248737341529));
#19763=CARTESIAN_POINT('Ctrl Pts',(1.12293169364966,1.69166666666666,1.94497474683058));
#19764=CARTESIAN_POINT('Ctrl Pts',(0.,1.75,1.94497474683058));
#19765=CARTESIAN_POINT('Ctrl Pts',(-1.12293169364966,1.80833333333333,1.94497474683058));
#19766=CARTESIAN_POINT('Ctrl Pts',(-1.68439754047449,1.86666666666666,0.972487373415292));
#19767=CARTESIAN_POINT('Ctrl Pts',(-2.24586338729932,1.925,1.37519470428917E-16));
#19768=CARTESIAN_POINT('Ctrl Pts',(-1.68439754047449,1.98333333333333,-0.972487373415291));
#19769=CARTESIAN_POINT('Ctrl Pts',(-1.12293169364966,2.04166666666666,-1.94497474683058));
#19770=CARTESIAN_POINT('Ctrl Pts',(-2.38190709812851E-16,2.1,-1.94497474683058));
#19771=CARTESIAN_POINT('Ctrl Pts',(1.12293169364966,2.15833333333333,-1.94497474683058));
#19772=CARTESIAN_POINT('Ctrl Pts',(1.68439754047449,2.21666666666666,-0.972487373415292));
#19773=CARTESIAN_POINT('Ctrl Pts',(2.24586338729932,2.275,-4.12558411286752E-16));
#19774=CARTESIAN_POINT('Ctrl Pts',(1.68439754047449,2.33333333333333,0.97248737341529));
#19775=CARTESIAN_POINT('Ctrl Pts',(1.12293169364966,2.39166666666666,1.94497474683058));
#19776=CARTESIAN_POINT('Ctrl Pts',(0.,2.45,1.94497474683058));
#19777=CARTESIAN_POINT('Ctrl Pts',(-1.12293169364966,2.50833333333333,1.94497474683058));
#19778=CARTESIAN_POINT('Ctrl Pts',(-1.68439754047449,2.56666666666666,0.972487373415292));
#19779=CARTESIAN_POINT('Ctrl Pts',(-2.24586338729932,2.62499999999999,1.37519470428917E-16));
#19780=CARTESIAN_POINT('Ctrl Pts',(-1.68439754047449,2.68333333333333,-0.972487373415291));
#19781=CARTESIAN_POINT('Ctrl Pts',(-1.12293169364966,2.74166666666666,-1.94497474683058));
#19782=CARTESIAN_POINT('Ctrl Pts',(-2.38190709812851E-16,2.8,-1.94497474683058));
#19783=CARTESIAN_POINT('Ctrl Pts',(1.12293169364966,2.85833333333333,-1.94497474683058));
#19784=CARTESIAN_POINT('Ctrl Pts',(1.68439754047449,2.91666666666666,-0.972487373415292));
#19785=CARTESIAN_POINT('Ctrl Pts',(2.24586338729932,2.97499999999999,-4.12558411286752E-16));
#19786=CARTESIAN_POINT('Ctrl Pts',(1.68439754047449,3.03333333333333,0.97248737341529));
#19787=CARTESIAN_POINT('Ctrl Pts',(1.12293169364966,3.09166666666666,1.94497474683058));
#19788=CARTESIAN_POINT('Ctrl Pts',(0.,3.14999999999999,1.94497474683058));
#19789=CARTESIAN_POINT('Ctrl Pts',(-1.12293169364966,3.20833333333333,1.94497474683058));
#19790=CARTESIAN_POINT('Ctrl Pts',(-1.68439754047449,3.26666666666666,0.972487373415292));
#19791=CARTESIAN_POINT('Ctrl Pts',(-2.24586338729932,3.32499999999999,1.37519470428917E-16));
#19792=CARTESIAN_POINT('Ctrl Pts',(-1.68439754047449,3.38333333333333,-0.972487373415291));
#19793=CARTESIAN_POINT('Ctrl Pts',(-1.12293169364966,3.44166666666666,-1.94497474683058));
#19794=CARTESIAN_POINT('Ctrl Pts',(-2.38190709812851E-16,3.49999999999999,
-1.94497474683058));
#19795=CARTESIAN_POINT('Ctrl Pts',(1.12293169364966,3.55833333333333,-1.94497474683058));
#19796=CARTESIAN_POINT('Ctrl Pts',(1.68439754047449,3.61666666666666,-0.972487373415292));
#19797=CARTESIAN_POINT('Ctrl Pts',(2.24586338729932,3.67499999999999,-4.12558411286752E-16));
#19798=CARTESIAN_POINT('Ctrl Pts',(1.68439754047449,3.73333333333333,0.97248737341529));
#19799=CARTESIAN_POINT('Ctrl Pts',(1.12293169364966,3.79166666666666,1.94497474683058));
#19800=CARTESIAN_POINT('Ctrl Pts',(0.,3.84999999999999,1.94497474683058));
#19801=CARTESIAN_POINT('Ctrl Pts',(-1.12293169364966,3.90833333333333,1.94497474683058));
#19802=CARTESIAN_POINT('Ctrl Pts',(-1.68439754047449,3.96666666666666,0.972487373415292));
#19803=CARTESIAN_POINT('Ctrl Pts',(-2.24586338729932,4.02499999999999,1.37519470428917E-16));
#19804=CARTESIAN_POINT('Ctrl Pts',(-1.68439754047449,4.08333333333333,-0.972487373415291));
#19805=CARTESIAN_POINT('Ctrl Pts',(-1.12293169364966,4.14166666666666,-1.94497474683058));
#19806=CARTESIAN_POINT('Ctrl Pts',(-2.38190709812851E-16,4.19999999999999,
-1.94497474683058));
#19807=CARTESIAN_POINT('Ctrl Pts',(1.12293169364966,4.25833333333332,-1.94497474683058));
#19808=CARTESIAN_POINT('Ctrl Pts',(1.68439754047449,4.31666666666666,-0.972487373415292));
#19809=CARTESIAN_POINT('Ctrl Pts',(2.24586338729932,4.37499999999999,-4.12558411286752E-16));
#19810=CARTESIAN_POINT('Ctrl Pts',(1.68439754047449,4.43333333333332,0.97248737341529));
#19811=CARTESIAN_POINT('Ctrl Pts',(1.12293169364966,4.49166666666666,1.94497474683058));
#19812=CARTESIAN_POINT('Ctrl Pts',(0.,4.54999999999999,1.94497474683058));
#19813=CARTESIAN_POINT('Ctrl Pts',(0.,0.35,2.15));
#19814=CARTESIAN_POINT('Ctrl Pts',(-1.2413030787577,0.408333333333333,2.15));
#19815=CARTESIAN_POINT('Ctrl Pts',(-1.86195461813654,0.466666666666667,
1.075));
#19816=CARTESIAN_POINT('Ctrl Pts',(-2.48260615751539,0.525,1.52015784217237E-16));
#19817=CARTESIAN_POINT('Ctrl Pts',(-1.86195461813654,0.583333333333333,
-1.075));
#19818=CARTESIAN_POINT('Ctrl Pts',(-1.2413030787577,0.641666666666666,-2.15));
#19819=CARTESIAN_POINT('Ctrl Pts',(-2.63299061816681E-16,0.699999999999999,
-2.15));
#19820=CARTESIAN_POINT('Ctrl Pts',(1.24130307875769,0.758333333333333,-2.15));
#19821=CARTESIAN_POINT('Ctrl Pts',(1.86195461813654,0.816666666666666,-1.075));
#19822=CARTESIAN_POINT('Ctrl Pts',(2.48260615751539,0.874999999999999,-4.5604735265171E-16));
#19823=CARTESIAN_POINT('Ctrl Pts',(1.86195461813654,0.933333333333332,1.075));
#19824=CARTESIAN_POINT('Ctrl Pts',(1.2413030787577,0.991666666666666,2.15));
#19825=CARTESIAN_POINT('Ctrl Pts',(0.,1.05,2.15));
#19826=CARTESIAN_POINT('Ctrl Pts',(-1.2413030787577,1.10833333333333,2.15));
#19827=CARTESIAN_POINT('Ctrl Pts',(-1.86195461813654,1.16666666666667,1.075));
#19828=CARTESIAN_POINT('Ctrl Pts',(-2.48260615751539,1.225,1.52015784217237E-16));
#19829=CARTESIAN_POINT('Ctrl Pts',(-1.86195461813654,1.28333333333333,-1.075));
#19830=CARTESIAN_POINT('Ctrl Pts',(-1.2413030787577,1.34166666666666,-2.15));
#19831=CARTESIAN_POINT('Ctrl Pts',(-2.63299061816681E-16,1.4,-2.15));
#19832=CARTESIAN_POINT('Ctrl Pts',(1.24130307875769,1.45833333333333,-2.15));
#19833=CARTESIAN_POINT('Ctrl Pts',(1.86195461813654,1.51666666666666,-1.075));
#19834=CARTESIAN_POINT('Ctrl Pts',(2.48260615751539,1.575,-4.5604735265171E-16));
#19835=CARTESIAN_POINT('Ctrl Pts',(1.86195461813654,1.63333333333333,1.075));
#19836=CARTESIAN_POINT('Ctrl Pts',(1.2413030787577,1.69166666666666,2.15));
#19837=CARTESIAN_POINT('Ctrl Pts',(0.,1.75,2.15));
#19838=CARTESIAN_POINT('Ctrl Pts',(-1.2413030787577,1.80833333333333,2.15));
#19839=CARTESIAN_POINT('Ctrl Pts',(-1.86195461813654,1.86666666666666,1.075));
#19840=CARTESIAN_POINT('Ctrl Pts',(-2.48260615751539,1.925,1.52015784217237E-16));
#19841=CARTESIAN_POINT('Ctrl Pts',(-1.86195461813654,1.98333333333333,-1.075));
#19842=CARTESIAN_POINT('Ctrl Pts',(-1.2413030787577,2.04166666666666,-2.15));
#19843=CARTESIAN_POINT('Ctrl Pts',(-2.63299061816681E-16,2.1,-2.15));
#19844=CARTESIAN_POINT('Ctrl Pts',(1.24130307875769,2.15833333333333,-2.15));
#19845=CARTESIAN_POINT('Ctrl Pts',(1.86195461813654,2.21666666666666,-1.075));
#19846=CARTESIAN_POINT('Ctrl Pts',(2.48260615751539,2.275,-4.5604735265171E-16));
#19847=CARTESIAN_POINT('Ctrl Pts',(1.86195461813654,2.33333333333333,1.075));
#19848=CARTESIAN_POINT('Ctrl Pts',(1.2413030787577,2.39166666666666,2.15));
#19849=CARTESIAN_POINT('Ctrl Pts',(0.,2.45,2.15));
#19850=CARTESIAN_POINT('Ctrl Pts',(-1.2413030787577,2.50833333333333,2.15));
#19851=CARTESIAN_POINT('Ctrl Pts',(-1.86195461813654,2.56666666666666,1.075));
#19852=CARTESIAN_POINT('Ctrl Pts',(-2.48260615751539,2.625,1.52015784217237E-16));
#19853=CARTESIAN_POINT('Ctrl Pts',(-1.86195461813654,2.68333333333333,-1.075));
#19854=CARTESIAN_POINT('Ctrl Pts',(-1.2413030787577,2.74166666666666,-2.15));
#19855=CARTESIAN_POINT('Ctrl Pts',(-2.63299061816681E-16,2.8,-2.15));
#19856=CARTESIAN_POINT('Ctrl Pts',(1.24130307875769,2.85833333333333,-2.15));
#19857=CARTESIAN_POINT('Ctrl Pts',(1.86195461813654,2.91666666666666,-1.075));
#19858=CARTESIAN_POINT('Ctrl Pts',(2.48260615751539,2.97499999999999,-4.5604735265171E-16));
#19859=CARTESIAN_POINT('Ctrl Pts',(1.86195461813654,3.03333333333333,1.075));
#19860=CARTESIAN_POINT('Ctrl Pts',(1.2413030787577,3.09166666666666,2.15));
#19861=CARTESIAN_POINT('Ctrl Pts',(0.,3.15,2.15));
#19862=CARTESIAN_POINT('Ctrl Pts',(-1.2413030787577,3.20833333333333,2.15));
#19863=CARTESIAN_POINT('Ctrl Pts',(-1.86195461813654,3.26666666666666,1.075));
#19864=CARTESIAN_POINT('Ctrl Pts',(-2.48260615751539,3.32499999999999,1.52015784217237E-16));
#19865=CARTESIAN_POINT('Ctrl Pts',(-1.86195461813654,3.38333333333333,-1.075));
#19866=CARTESIAN_POINT('Ctrl Pts',(-1.2413030787577,3.44166666666666,-2.15));
#19867=CARTESIAN_POINT('Ctrl Pts',(-2.63299061816681E-16,3.49999999999999,
-2.15));
#19868=CARTESIAN_POINT('Ctrl Pts',(1.24130307875769,3.55833333333333,-2.15));
#19869=CARTESIAN_POINT('Ctrl Pts',(1.86195461813654,3.61666666666666,-1.075));
#19870=CARTESIAN_POINT('Ctrl Pts',(2.48260615751539,3.67499999999999,-4.5604735265171E-16));
#19871=CARTESIAN_POINT('Ctrl Pts',(1.86195461813654,3.73333333333333,1.075));
#19872=CARTESIAN_POINT('Ctrl Pts',(1.2413030787577,3.79166666666666,2.15));
#19873=CARTESIAN_POINT('Ctrl Pts',(0.,3.84999999999999,2.15));
#19874=CARTESIAN_POINT('Ctrl Pts',(-1.2413030787577,3.90833333333333,2.15));
#19875=CARTESIAN_POINT('Ctrl Pts',(-1.86195461813654,3.96666666666666,1.075));
#19876=CARTESIAN_POINT('Ctrl Pts',(-2.48260615751539,4.02499999999999,1.52015784217237E-16));
#19877=CARTESIAN_POINT('Ctrl Pts',(-1.86195461813654,4.08333333333333,-1.075));
#19878=CARTESIAN_POINT('Ctrl Pts',(-1.2413030787577,4.14166666666666,-2.15));
#19879=CARTESIAN_POINT('Ctrl Pts',(-2.63299061816681E-16,4.19999999999999,
-2.15));
#19880=CARTESIAN_POINT('Ctrl Pts',(1.24130307875769,4.25833333333333,-2.15));
#19881=CARTESIAN_POINT('Ctrl Pts',(1.86195461813654,4.31666666666666,-1.075));
#19882=CARTESIAN_POINT('Ctrl Pts',(2.48260615751539,4.37499999999999,-4.5604735265171E-16));
#19883=CARTESIAN_POINT('Ctrl Pts',(1.86195461813654,4.43333333333333,1.075));
#19884=CARTESIAN_POINT('Ctrl Pts',(1.2413030787577,4.49166666666666,2.15));
#19885=CARTESIAN_POINT('Ctrl Pts',(0.,4.54999999999999,2.15));
#19886=CARTESIAN_POINT('',(-7.40933783759325E-14,4.2,1.8));
#19887=CARTESIAN_POINT('',(-8.82371251094361E-14,4.55,2.15));
#19888=CARTESIAN_POINT('Origin',(-1.80160437084306E-13,4.2,2.15));
#19889=CARTESIAN_POINT('',(-8.87637232330694E-14,3.85,2.15));
#19890=CARTESIAN_POINT('Ctrl Pts',(1.05346240894046E-14,3.84999999999999,
2.15));
#19891=CARTESIAN_POINT('Ctrl Pts',(-1.24130307875769,3.90833333333333,2.15));
#19892=CARTESIAN_POINT('Ctrl Pts',(-1.86195461813654,3.96666666666666,1.075));
#19893=CARTESIAN_POINT('Ctrl Pts',(-2.48260615751539,4.02499999999999,1.67263463193154E-14));
#19894=CARTESIAN_POINT('Ctrl Pts',(-1.86195461813655,4.08333333333333,-1.07499999999999));
#19895=CARTESIAN_POINT('Ctrl Pts',(-1.2413030787577,4.14166666666666,-2.15));
#19896=CARTESIAN_POINT('Ctrl Pts',(-1.07979231512212E-14,4.19999999999999,
-2.15));
#19897=CARTESIAN_POINT('Ctrl Pts',(1.24130307875769,4.25833333333332,-2.15));
#19898=CARTESIAN_POINT('Ctrl Pts',(1.86195461813654,4.31666666666666,-1.07500000000001));
#19899=CARTESIAN_POINT('Ctrl Pts',(2.48260615751539,4.37499999999999,-8.21038903287055E-15));
#19900=CARTESIAN_POINT('Ctrl Pts',(1.86195461813655,4.43333333333332,1.07499999999999));
#19901=CARTESIAN_POINT('Ctrl Pts',(1.24130307875771,4.49166666666666,2.14999999999999));
#19902=CARTESIAN_POINT('Ctrl Pts',(-8.82371251094361E-14,4.55,2.15));
#19903=CARTESIAN_POINT('',(2.63299061816681E-16,0.349999999999999,2.15));
#19904=CARTESIAN_POINT('Ctrl Pts',(2.63299061816681E-16,0.349999999999999,
2.15));
#19905=CARTESIAN_POINT('Ctrl Pts',(-1.24130307875769,0.408333333333333,
2.15));
#19906=CARTESIAN_POINT('Ctrl Pts',(-1.86195461813654,0.466666666666666,
1.075));
#19907=CARTESIAN_POINT('Ctrl Pts',(-2.48260615751539,0.524999999999999,
4.5604735265171E-16));
#19908=CARTESIAN_POINT('Ctrl Pts',(-1.86195461813654,0.583333333333332,
-1.075));
#19909=CARTESIAN_POINT('Ctrl Pts',(-1.2413030787577,0.641666666666665,-2.15));
#19910=CARTESIAN_POINT('Ctrl Pts',(-5.26598123633362E-16,0.699999999999999,
-2.15));
#19911=CARTESIAN_POINT('Ctrl Pts',(1.24130307875769,0.758333333333332,-2.15));
#19912=CARTESIAN_POINT('Ctrl Pts',(1.86195461813654,0.816666666666665,-1.075));
#19913=CARTESIAN_POINT('Ctrl Pts',(2.48260615751539,0.874999999999999,-7.60078921086183E-16));
#19914=CARTESIAN_POINT('Ctrl Pts',(1.86195461813654,0.933333333333332,1.075));
#19915=CARTESIAN_POINT('Ctrl Pts',(1.2413030787577,0.991666666666665,2.15));
#19916=CARTESIAN_POINT('Ctrl Pts',(7.89897185450043E-16,1.05,2.15));
#19917=CARTESIAN_POINT('Ctrl Pts',(-1.24130307875769,1.10833333333333,2.15));
#19918=CARTESIAN_POINT('Ctrl Pts',(-1.86195461813654,1.16666666666666,1.075));
#19919=CARTESIAN_POINT('Ctrl Pts',(-2.48260615751539,1.225,3.26910770324048E-15));
#19920=CARTESIAN_POINT('Ctrl Pts',(-1.86195461813654,1.28333333333333,-1.075));
#19921=CARTESIAN_POINT('Ctrl Pts',(-1.2413030787577,1.34166666666666,-2.15));
#19922=CARTESIAN_POINT('Ctrl Pts',(-1.05319624726672E-15,1.4,-2.15));
#19923=CARTESIAN_POINT('Ctrl Pts',(1.24130307875769,1.45833333333333,-2.15));
#19924=CARTESIAN_POINT('Ctrl Pts',(1.86195461813654,1.51666666666666,-1.075));
#19925=CARTESIAN_POINT('Ctrl Pts',(2.48260615751539,1.575,-1.36814205795513E-15));
#19926=CARTESIAN_POINT('Ctrl Pts',(1.86195461813654,1.63333333333333,1.075));
#19927=CARTESIAN_POINT('Ctrl Pts',(1.2413030787577,1.69166666666666,2.15));
#19928=CARTESIAN_POINT('Ctrl Pts',(1.3164953090834E-15,1.75,2.15));
#19929=CARTESIAN_POINT('Ctrl Pts',(-1.24130307875769,1.80833333333333,2.15));
#19930=CARTESIAN_POINT('Ctrl Pts',(-1.86195461813654,1.86666666666666,1.075));
#19931=CARTESIAN_POINT('Ctrl Pts',(-2.48260615751539,1.925,6.08216805382924E-15));
#19932=CARTESIAN_POINT('Ctrl Pts',(-1.86195461813654,1.98333333333333,-1.075));
#19933=CARTESIAN_POINT('Ctrl Pts',(-1.2413030787577,2.04166666666666,-2.15));
#19934=CARTESIAN_POINT('Ctrl Pts',(-5.39896157561062E-15,2.1,-2.15));
#19935=CARTESIAN_POINT('Ctrl Pts',(1.24130307875769,2.15833333333333,-2.15));
#19936=CARTESIAN_POINT('Ctrl Pts',(1.86195461813654,2.21666666666666,-1.075));
#19937=CARTESIAN_POINT('Ctrl Pts',(2.48260615751539,2.275,-6.38619962226372E-15));
#19938=CARTESIAN_POINT('Ctrl Pts',(1.86195461813655,2.33333333333333,1.07499999999999));
#19939=CARTESIAN_POINT('Ctrl Pts',(1.2413030787577,2.39166666666666,2.15));
#19940=CARTESIAN_POINT('Ctrl Pts',(1.84309343271677E-15,2.45,2.15));
#19941=CARTESIAN_POINT('Ctrl Pts',(-1.24130307875769,2.50833333333333,2.15));
#19942=CARTESIAN_POINT('Ctrl Pts',(-1.86195461813654,2.56666666666666,1.075));
#19943=CARTESIAN_POINT('Ctrl Pts',(-2.48260615751539,2.62499999999999,6.69023119069819E-15));
#19944=CARTESIAN_POINT('Ctrl Pts',(-1.86195461813655,2.68333333333333,-1.07499999999999));
#19945=CARTESIAN_POINT('Ctrl Pts',(-1.2413030787577,2.74166666666666,-2.14999999999999));
#19946=CARTESIAN_POINT('Ctrl Pts',(-2.10639249453345E-15,2.79999999999999,
-2.15));
#19947=CARTESIAN_POINT('Ctrl Pts',(1.24130307875769,2.85833333333333,-2.15));
#19948=CARTESIAN_POINT('Ctrl Pts',(1.86195461813654,2.91666666666666,-1.075));
#19949=CARTESIAN_POINT('Ctrl Pts',(2.48260615751539,2.97499999999999,-6.99426275913266E-15));
#19950=CARTESIAN_POINT('Ctrl Pts',(1.86195461813655,3.03333333333333,1.07499999999999));
#19951=CARTESIAN_POINT('Ctrl Pts',(1.2413030787577,3.09166666666666,2.14999999999999));
#19952=CARTESIAN_POINT('Ctrl Pts',(2.36969155635013E-15,3.14999999999999,
2.15));
#19953=CARTESIAN_POINT('Ctrl Pts',(-1.24130307875769,3.20833333333333,2.15));
#19954=CARTESIAN_POINT('Ctrl Pts',(-1.86195461813654,3.26666666666666,1.075));
#19955=CARTESIAN_POINT('Ctrl Pts',(-2.48260615751539,3.32499999999999,7.29829432756713E-15));
#19956=CARTESIAN_POINT('Ctrl Pts',(-1.86195461813655,3.38333333333333,-1.07499999999999));
#19957=CARTESIAN_POINT('Ctrl Pts',(-1.2413030787577,3.44166666666666,-2.14999999999999));
#19958=CARTESIAN_POINT('Ctrl Pts',(-1.02713250275879E-14,3.49999999999999,
-2.15));
#19959=CARTESIAN_POINT('Ctrl Pts',(1.24130307875769,3.55833333333333,-2.15));
#19960=CARTESIAN_POINT('Ctrl Pts',(1.86195461813654,3.61666666666666,-1.075));
#19961=CARTESIAN_POINT('Ctrl Pts',(2.48260615751539,3.67499999999999,-7.60232589600161E-15));
#19962=CARTESIAN_POINT('Ctrl Pts',(1.86195461813655,3.73333333333333,1.07499999999999));
#19963=CARTESIAN_POINT('Ctrl Pts',(1.2413030787577,3.79166666666666,2.14999999999999));
#19964=CARTESIAN_POINT('Ctrl Pts',(1.05346240894046E-14,3.84999999999999,
2.15));
#19965=CARTESIAN_POINT('',(0.,0.,1.8));
#19966=CARTESIAN_POINT('Origin',(0.,0.,2.15));
#19967=CARTESIAN_POINT('Ctrl Pts',(0.,0.,1.8));
#19968=CARTESIAN_POINT('Ctrl Pts',(-1.03923048454133,0.0583333333333332,
1.8));
#19969=CARTESIAN_POINT('Ctrl Pts',(-1.55884572681199,0.116666666666666,
0.9));
#19970=CARTESIAN_POINT('Ctrl Pts',(-2.07846096908265,0.175,1.27269028646989E-16));
#19971=CARTESIAN_POINT('Ctrl Pts',(-1.55884572681199,0.233333333333333,
-0.9));
#19972=CARTESIAN_POINT('Ctrl Pts',(-1.03923048454133,0.291666666666666,
-1.8));
#19973=CARTESIAN_POINT('Ctrl Pts',(-2.20436423846524E-16,0.349999999999999,
-1.8));
#19974=CARTESIAN_POINT('Ctrl Pts',(1.03923048454133,0.408333333333333,-1.8));
#19975=CARTESIAN_POINT('Ctrl Pts',(1.55884572681199,0.466666666666666,-0.900000000000001));
#19976=CARTESIAN_POINT('Ctrl Pts',(2.07846096908265,0.524999999999999,-3.81807085940967E-16));
#19977=CARTESIAN_POINT('Ctrl Pts',(1.55884572681199,0.583333333333332,0.899999999999999));
#19978=CARTESIAN_POINT('Ctrl Pts',(1.03923048454133,0.641666666666665,1.8));
#19979=CARTESIAN_POINT('Ctrl Pts',(4.40872847693047E-16,0.699999999999999,
1.8));
#19980=CARTESIAN_POINT('Ctrl Pts',(-1.03923048454132,0.758333333333332,
1.8));
#19981=CARTESIAN_POINT('Ctrl Pts',(-1.55884572681199,0.816666666666665,
0.900000000000001));
#19982=CARTESIAN_POINT('Ctrl Pts',(-2.07846096908265,0.874999999999998,
2.48238932216317E-15));
#19983=CARTESIAN_POINT('Ctrl Pts',(-1.55884572681199,0.933333333333332,
-0.899999999999999));
#19984=CARTESIAN_POINT('Ctrl Pts',(-1.03923048454133,0.991666666666665,
-1.8));
#19985=CARTESIAN_POINT('Ctrl Pts',(-6.61309271539571E-16,1.05,-1.8));
#19986=CARTESIAN_POINT('Ctrl Pts',(1.03923048454132,1.10833333333333,-1.8));
#19987=CARTESIAN_POINT('Ctrl Pts',(1.55884572681199,1.16666666666666,-0.900000000000002));
#19988=CARTESIAN_POINT('Ctrl Pts',(2.07846096908265,1.225,-8.90883200528922E-16));
#19989=CARTESIAN_POINT('Ctrl Pts',(1.55884572681199,1.28333333333333,0.899999999999998));
#19990=CARTESIAN_POINT('Ctrl Pts',(1.03923048454133,1.34166666666666,1.8));
#19991=CARTESIAN_POINT('Ctrl Pts',(8.81745695386094E-16,1.4,1.8));
#19992=CARTESIAN_POINT('Ctrl Pts',(-1.03923048454132,1.45833333333333,1.8));
#19993=CARTESIAN_POINT('Ctrl Pts',(-1.55884572681199,1.51666666666666,0.900000000000003));
#19994=CARTESIAN_POINT('Ctrl Pts',(-2.07846096908265,1.575,4.83750961567934E-15));
#19995=CARTESIAN_POINT('Ctrl Pts',(-1.55884572681199,1.63333333333333,-0.899999999999998));
#19996=CARTESIAN_POINT('Ctrl Pts',(-1.03923048454133,1.69166666666666,-1.8));
#19997=CARTESIAN_POINT('Ctrl Pts',(-4.29962443015307E-15,1.75,-1.8));
#19998=CARTESIAN_POINT('Ctrl Pts',(1.03923048454132,1.80833333333333,-1.8));
#19999=CARTESIAN_POINT('Ctrl Pts',(1.55884572681199,1.86666666666666,-0.900000000000003));
#20000=CARTESIAN_POINT('Ctrl Pts',(2.07846096908265,1.925,-5.09204767297332E-15));
#20001=CARTESIAN_POINT('Ctrl Pts',(1.55884572681199,1.98333333333333,0.899999999999995));
#20002=CARTESIAN_POINT('Ctrl Pts',(1.03923048454133,2.04166666666666,1.8));
#20003=CARTESIAN_POINT('Ctrl Pts',(1.32261854307914E-15,2.1,1.8));
#20004=CARTESIAN_POINT('Ctrl Pts',(-1.03923048454132,2.15833333333333,1.8));
#20005=CARTESIAN_POINT('Ctrl Pts',(-1.55884572681199,2.21666666666666,0.900000000000003));
#20006=CARTESIAN_POINT('Ctrl Pts',(-2.07846096908265,2.275,5.3465857302673E-15));
#20007=CARTESIAN_POINT('Ctrl Pts',(-1.55884572681199,2.33333333333333,-0.899999999999995));
#20008=CARTESIAN_POINT('Ctrl Pts',(-1.03923048454133,2.39166666666666,-1.8));
#20009=CARTESIAN_POINT('Ctrl Pts',(-1.54305496692567E-15,2.45,-1.8));
#20010=CARTESIAN_POINT('Ctrl Pts',(1.03923048454132,2.50833333333333,-1.8));
#20011=CARTESIAN_POINT('Ctrl Pts',(1.55884572681199,2.56666666666666,-0.900000000000003));
#20012=CARTESIAN_POINT('Ctrl Pts',(2.07846096908265,2.625,-5.60112378756128E-15));
#20013=CARTESIAN_POINT('Ctrl Pts',(1.55884572681199,2.68333333333333,0.899999999999995));
#20014=CARTESIAN_POINT('Ctrl Pts',(1.03923048454133,2.74166666666666,1.8));
#20015=CARTESIAN_POINT('Ctrl Pts',(1.76349139077219E-15,2.79999999999999,
1.8));
#20016=CARTESIAN_POINT('Ctrl Pts',(-1.03923048454132,2.85833333333333,1.8));
#20017=CARTESIAN_POINT('Ctrl Pts',(-1.55884572681199,2.91666666666666,0.900000000000003));
#20018=CARTESIAN_POINT('Ctrl Pts',(-2.07846096908265,2.97499999999999,5.85566184485525E-15));
#20019=CARTESIAN_POINT('Ctrl Pts',(-1.55884572681199,3.03333333333333,-0.899999999999995));
#20020=CARTESIAN_POINT('Ctrl Pts',(-1.03923048454133,3.09166666666666,-1.8));
#20021=CARTESIAN_POINT('Ctrl Pts',(-8.37881243645961E-15,3.14999999999999,
-1.8));
#20022=CARTESIAN_POINT('Ctrl Pts',(1.03923048454132,3.20833333333333,-1.8));
#20023=CARTESIAN_POINT('Ctrl Pts',(1.55884572681199,3.26666666666666,-0.900000000000004));
#20024=CARTESIAN_POINT('Ctrl Pts',(2.07846096908265,3.32499999999999,-6.11019990214923E-15));
#20025=CARTESIAN_POINT('Ctrl Pts',(1.55884572681199,3.38333333333333,0.899999999999995));
#20026=CARTESIAN_POINT('Ctrl Pts',(1.03923048454133,3.44166666666666,1.8));
#20027=CARTESIAN_POINT('Ctrl Pts',(8.59924886030614E-15,3.49999999999999,
1.8));
#20028=CARTESIAN_POINT('Ctrl Pts',(-1.03923048454132,3.55833333333333,1.8));
#20029=CARTESIAN_POINT('Ctrl Pts',(-1.55884572681199,3.61666666666666,0.900000000000004));
#20030=CARTESIAN_POINT('Ctrl Pts',(-2.07846096908265,3.67499999999999,1.37489146751561E-14));
#20031=CARTESIAN_POINT('Ctrl Pts',(-1.55884572681199,3.73333333333333,-0.899999999999994));
#20032=CARTESIAN_POINT('Ctrl Pts',(-1.03923048454133,3.79166666666666,-1.8));
#20033=CARTESIAN_POINT('Ctrl Pts',(-8.81968528415266E-15,3.84999999999999,
-1.8));
#20034=CARTESIAN_POINT('Ctrl Pts',(1.03923048454132,3.90833333333333,-1.8));
#20035=CARTESIAN_POINT('Ctrl Pts',(1.55884572681198,3.96666666666666,-0.90000000000001));
#20036=CARTESIAN_POINT('Ctrl Pts',(2.07846096908265,4.02499999999999,-6.61927601673719E-15));
#20037=CARTESIAN_POINT('Ctrl Pts',(1.558845726812,4.08333333333333,0.899999999999989));
#20038=CARTESIAN_POINT('Ctrl Pts',(1.03923048454133,4.14166666666666,1.8));
#20039=CARTESIAN_POINT('Ctrl Pts',(-7.40933783759325E-14,4.2,1.8));
#20040=CARTESIAN_POINT('Ctrl Pts',(0.,-0.35,2.15));
#20041=CARTESIAN_POINT('Ctrl Pts',(-1.2413030787577,-0.291666666666667,
2.15));
#20042=CARTESIAN_POINT('Ctrl Pts',(-1.86195461813654,-0.233333333333334,
1.075));
#20043=CARTESIAN_POINT('Ctrl Pts',(-2.48260615751539,-0.175,1.52015784217237E-16));
#20044=CARTESIAN_POINT('Ctrl Pts',(-1.86195461813654,-0.116666666666667,
-1.075));
#20045=CARTESIAN_POINT('Ctrl Pts',(-1.2413030787577,-0.058333333333334,
-2.15));
#20046=CARTESIAN_POINT('Ctrl Pts',(-2.63299061816681E-16,-7.58941520739853E-16,
-2.15));
#20047=CARTESIAN_POINT('Ctrl Pts',(1.24130307875769,0.0583333333333325,
-2.15));
#20048=CARTESIAN_POINT('Ctrl Pts',(1.86195461813654,0.116666666666666,-1.075));
#20049=CARTESIAN_POINT('Ctrl Pts',(2.48260615751539,0.174999999999999,-4.5604735265171E-16));
#20050=CARTESIAN_POINT('Ctrl Pts',(1.86195461813654,0.233333333333332,1.075));
#20051=CARTESIAN_POINT('Ctrl Pts',(1.2413030787577,0.291666666666665,2.15));
#20052=CARTESIAN_POINT('Ctrl Pts',(0.,0.349999999999999,2.15));
#20053=CARTESIAN_POINT('Ctrl Pts',(-1.2413030787577,0.408333333333332,2.15));
#20054=CARTESIAN_POINT('Ctrl Pts',(-1.86195461813654,0.466666666666665,
1.075));
#20055=CARTESIAN_POINT('Ctrl Pts',(-2.48260615751539,0.524999999999998,
1.52015784217237E-16));
#20056=CARTESIAN_POINT('Ctrl Pts',(-1.86195461813654,0.583333333333331,
-1.075));
#20057=CARTESIAN_POINT('Ctrl Pts',(-1.2413030787577,0.641666666666665,-2.15));
#20058=CARTESIAN_POINT('Ctrl Pts',(-2.63299061816681E-16,0.699999999999998,
-2.15));
#20059=CARTESIAN_POINT('Ctrl Pts',(1.24130307875769,0.758333333333331,-2.15));
#20060=CARTESIAN_POINT('Ctrl Pts',(1.86195461813654,0.816666666666664,-1.075));
#20061=CARTESIAN_POINT('Ctrl Pts',(2.48260615751539,0.874999999999997,-4.5604735265171E-16));
#20062=CARTESIAN_POINT('Ctrl Pts',(1.86195461813654,0.933333333333331,1.075));
#20063=CARTESIAN_POINT('Ctrl Pts',(1.2413030787577,0.991666666666664,2.15));
#20064=CARTESIAN_POINT('Ctrl Pts',(0.,1.05,2.15));
#20065=CARTESIAN_POINT('Ctrl Pts',(-1.2413030787577,1.10833333333333,2.15));
#20066=CARTESIAN_POINT('Ctrl Pts',(-1.86195461813654,1.16666666666666,1.075));
#20067=CARTESIAN_POINT('Ctrl Pts',(-2.48260615751539,1.225,1.52015784217237E-16));
#20068=CARTESIAN_POINT('Ctrl Pts',(-1.86195461813654,1.28333333333333,-1.075));
#20069=CARTESIAN_POINT('Ctrl Pts',(-1.2413030787577,1.34166666666666,-2.15));
#20070=CARTESIAN_POINT('Ctrl Pts',(-2.63299061816681E-16,1.4,-2.15));
#20071=CARTESIAN_POINT('Ctrl Pts',(1.24130307875769,1.45833333333333,-2.15));
#20072=CARTESIAN_POINT('Ctrl Pts',(1.86195461813654,1.51666666666666,-1.075));
#20073=CARTESIAN_POINT('Ctrl Pts',(2.48260615751539,1.575,-4.5604735265171E-16));
#20074=CARTESIAN_POINT('Ctrl Pts',(1.86195461813654,1.63333333333333,1.075));
#20075=CARTESIAN_POINT('Ctrl Pts',(1.2413030787577,1.69166666666666,2.15));
#20076=CARTESIAN_POINT('Ctrl Pts',(0.,1.75,2.15));
#20077=CARTESIAN_POINT('Ctrl Pts',(-1.2413030787577,1.80833333333333,2.15));
#20078=CARTESIAN_POINT('Ctrl Pts',(-1.86195461813654,1.86666666666666,1.075));
#20079=CARTESIAN_POINT('Ctrl Pts',(-2.48260615751539,1.925,1.52015784217237E-16));
#20080=CARTESIAN_POINT('Ctrl Pts',(-1.86195461813654,1.98333333333333,-1.075));
#20081=CARTESIAN_POINT('Ctrl Pts',(-1.2413030787577,2.04166666666666,-2.15));
#20082=CARTESIAN_POINT('Ctrl Pts',(-2.63299061816681E-16,2.1,-2.15));
#20083=CARTESIAN_POINT('Ctrl Pts',(1.24130307875769,2.15833333333333,-2.15));
#20084=CARTESIAN_POINT('Ctrl Pts',(1.86195461813654,2.21666666666666,-1.075));
#20085=CARTESIAN_POINT('Ctrl Pts',(2.48260615751539,2.275,-4.5604735265171E-16));
#20086=CARTESIAN_POINT('Ctrl Pts',(1.86195461813654,2.33333333333333,1.075));
#20087=CARTESIAN_POINT('Ctrl Pts',(1.2413030787577,2.39166666666666,2.15));
#20088=CARTESIAN_POINT('Ctrl Pts',(0.,2.44999999999999,2.15));
#20089=CARTESIAN_POINT('Ctrl Pts',(-1.2413030787577,2.50833333333333,2.15));
#20090=CARTESIAN_POINT('Ctrl Pts',(-1.86195461813654,2.56666666666666,1.075));
#20091=CARTESIAN_POINT('Ctrl Pts',(-2.48260615751539,2.62499999999999,1.52015784217237E-16));
#20092=CARTESIAN_POINT('Ctrl Pts',(-1.86195461813654,2.68333333333333,-1.075));
#20093=CARTESIAN_POINT('Ctrl Pts',(-1.2413030787577,2.74166666666666,-2.15));
#20094=CARTESIAN_POINT('Ctrl Pts',(-2.63299061816681E-16,2.79999999999999,
-2.15));
#20095=CARTESIAN_POINT('Ctrl Pts',(1.24130307875769,2.85833333333333,-2.15));
#20096=CARTESIAN_POINT('Ctrl Pts',(1.86195461813654,2.91666666666666,-1.075));
#20097=CARTESIAN_POINT('Ctrl Pts',(2.48260615751539,2.97499999999999,-4.5604735265171E-16));
#20098=CARTESIAN_POINT('Ctrl Pts',(1.86195461813654,3.03333333333333,1.075));
#20099=CARTESIAN_POINT('Ctrl Pts',(1.2413030787577,3.09166666666666,2.15));
#20100=CARTESIAN_POINT('Ctrl Pts',(0.,3.14999999999999,2.15));
#20101=CARTESIAN_POINT('Ctrl Pts',(-1.2413030787577,3.20833333333333,2.15));
#20102=CARTESIAN_POINT('Ctrl Pts',(-1.86195461813654,3.26666666666666,1.075));
#20103=CARTESIAN_POINT('Ctrl Pts',(-2.48260615751539,3.32499999999999,1.52015784217237E-16));
#20104=CARTESIAN_POINT('Ctrl Pts',(-1.86195461813654,3.38333333333333,-1.075));
#20105=CARTESIAN_POINT('Ctrl Pts',(-1.2413030787577,3.44166666666666,-2.15));
#20106=CARTESIAN_POINT('Ctrl Pts',(-2.63299061816681E-16,3.49999999999999,
-2.15));
#20107=CARTESIAN_POINT('Ctrl Pts',(1.24130307875769,3.55833333333333,-2.15));
#20108=CARTESIAN_POINT('Ctrl Pts',(1.86195461813654,3.61666666666666,-1.075));
#20109=CARTESIAN_POINT('Ctrl Pts',(2.48260615751539,3.67499999999999,-4.5604735265171E-16));
#20110=CARTESIAN_POINT('Ctrl Pts',(1.86195461813654,3.73333333333333,1.075));
#20111=CARTESIAN_POINT('Ctrl Pts',(1.2413030787577,3.79166666666666,2.15));
#20112=CARTESIAN_POINT('Ctrl Pts',(0.,3.84999999999999,2.15));
#20113=CARTESIAN_POINT('Ctrl Pts',(0.,-0.35,1.94497474683058));
#20114=CARTESIAN_POINT('Ctrl Pts',(-1.12293169364966,-0.291666666666667,
1.94497474683058));
#20115=CARTESIAN_POINT('Ctrl Pts',(-1.68439754047449,-0.233333333333334,
0.972487373415292));
#20116=CARTESIAN_POINT('Ctrl Pts',(-2.24586338729932,-0.175,1.37519470428917E-16));
#20117=CARTESIAN_POINT('Ctrl Pts',(-1.68439754047449,-0.116666666666667,
-0.972487373415291));
#20118=CARTESIAN_POINT('Ctrl Pts',(-1.12293169364966,-0.058333333333334,
-1.94497474683058));
#20119=CARTESIAN_POINT('Ctrl Pts',(-2.38190709812851E-16,-8.13151629364128E-16,
-1.94497474683058));
#20120=CARTESIAN_POINT('Ctrl Pts',(1.12293169364966,0.0583333333333324,
-1.94497474683058));
#20121=CARTESIAN_POINT('Ctrl Pts',(1.68439754047449,0.116666666666666,-0.972487373415292));
#20122=CARTESIAN_POINT('Ctrl Pts',(2.24586338729932,0.174999999999999,-4.12558411286752E-16));
#20123=CARTESIAN_POINT('Ctrl Pts',(1.68439754047449,0.233333333333332,0.97248737341529));
#20124=CARTESIAN_POINT('Ctrl Pts',(1.12293169364966,0.291666666666665,1.94497474683058));
#20125=CARTESIAN_POINT('Ctrl Pts',(0.,0.349999999999998,1.94497474683058));
#20126=CARTESIAN_POINT('Ctrl Pts',(-1.12293169364966,0.408333333333332,
1.94497474683058));
#20127=CARTESIAN_POINT('Ctrl Pts',(-1.68439754047449,0.466666666666665,
0.972487373415292));
#20128=CARTESIAN_POINT('Ctrl Pts',(-2.24586338729932,0.524999999999998,
1.37519470428917E-16));
#20129=CARTESIAN_POINT('Ctrl Pts',(-1.68439754047449,0.583333333333331,
-0.972487373415291));
#20130=CARTESIAN_POINT('Ctrl Pts',(-1.12293169364966,0.641666666666665,
-1.94497474683058));
#20131=CARTESIAN_POINT('Ctrl Pts',(-2.38190709812851E-16,0.699999999999998,
-1.94497474683058));
#20132=CARTESIAN_POINT('Ctrl Pts',(1.12293169364966,0.758333333333331,-1.94497474683058));
#20133=CARTESIAN_POINT('Ctrl Pts',(1.68439754047449,0.816666666666664,-0.972487373415292));
#20134=CARTESIAN_POINT('Ctrl Pts',(2.24586338729932,0.874999999999998,-4.12558411286752E-16));
#20135=CARTESIAN_POINT('Ctrl Pts',(1.68439754047449,0.933333333333331,0.97248737341529));
#20136=CARTESIAN_POINT('Ctrl Pts',(1.12293169364966,0.991666666666664,1.94497474683058));
#20137=CARTESIAN_POINT('Ctrl Pts',(0.,1.05,1.94497474683058));
#20138=CARTESIAN_POINT('Ctrl Pts',(-1.12293169364966,1.10833333333333,1.94497474683058));
#20139=CARTESIAN_POINT('Ctrl Pts',(-1.68439754047449,1.16666666666666,0.972487373415292));
#20140=CARTESIAN_POINT('Ctrl Pts',(-2.24586338729932,1.225,1.37519470428917E-16));
#20141=CARTESIAN_POINT('Ctrl Pts',(-1.68439754047449,1.28333333333333,-0.972487373415291));
#20142=CARTESIAN_POINT('Ctrl Pts',(-1.12293169364966,1.34166666666666,-1.94497474683058));
#20143=CARTESIAN_POINT('Ctrl Pts',(-2.38190709812851E-16,1.4,-1.94497474683058));
#20144=CARTESIAN_POINT('Ctrl Pts',(1.12293169364966,1.45833333333333,-1.94497474683058));
#20145=CARTESIAN_POINT('Ctrl Pts',(1.68439754047449,1.51666666666666,-0.972487373415292));
#20146=CARTESIAN_POINT('Ctrl Pts',(2.24586338729932,1.575,-4.12558411286752E-16));
#20147=CARTESIAN_POINT('Ctrl Pts',(1.68439754047449,1.63333333333333,0.97248737341529));
#20148=CARTESIAN_POINT('Ctrl Pts',(1.12293169364966,1.69166666666666,1.94497474683058));
#20149=CARTESIAN_POINT('Ctrl Pts',(0.,1.75,1.94497474683058));
#20150=CARTESIAN_POINT('Ctrl Pts',(-1.12293169364966,1.80833333333333,1.94497474683058));
#20151=CARTESIAN_POINT('Ctrl Pts',(-1.68439754047449,1.86666666666666,0.972487373415292));
#20152=CARTESIAN_POINT('Ctrl Pts',(-2.24586338729932,1.925,1.37519470428917E-16));
#20153=CARTESIAN_POINT('Ctrl Pts',(-1.68439754047449,1.98333333333333,-0.972487373415291));
#20154=CARTESIAN_POINT('Ctrl Pts',(-1.12293169364966,2.04166666666666,-1.94497474683058));
#20155=CARTESIAN_POINT('Ctrl Pts',(-2.38190709812851E-16,2.09999999999999,
-1.94497474683058));
#20156=CARTESIAN_POINT('Ctrl Pts',(1.12293169364966,2.15833333333333,-1.94497474683058));
#20157=CARTESIAN_POINT('Ctrl Pts',(1.68439754047449,2.21666666666666,-0.972487373415292));
#20158=CARTESIAN_POINT('Ctrl Pts',(2.24586338729932,2.275,-4.12558411286752E-16));
#20159=CARTESIAN_POINT('Ctrl Pts',(1.68439754047449,2.33333333333333,0.97248737341529));
#20160=CARTESIAN_POINT('Ctrl Pts',(1.12293169364966,2.39166666666666,1.94497474683058));
#20161=CARTESIAN_POINT('Ctrl Pts',(0.,2.44999999999999,1.94497474683058));
#20162=CARTESIAN_POINT('Ctrl Pts',(-1.12293169364966,2.50833333333333,1.94497474683058));
#20163=CARTESIAN_POINT('Ctrl Pts',(-1.68439754047449,2.56666666666666,0.972487373415292));
#20164=CARTESIAN_POINT('Ctrl Pts',(-2.24586338729932,2.62499999999999,1.37519470428917E-16));
#20165=CARTESIAN_POINT('Ctrl Pts',(-1.68439754047449,2.68333333333333,-0.972487373415291));
#20166=CARTESIAN_POINT('Ctrl Pts',(-1.12293169364966,2.74166666666666,-1.94497474683058));
#20167=CARTESIAN_POINT('Ctrl Pts',(-2.38190709812851E-16,2.79999999999999,
-1.94497474683058));
#20168=CARTESIAN_POINT('Ctrl Pts',(1.12293169364966,2.85833333333333,-1.94497474683058));
#20169=CARTESIAN_POINT('Ctrl Pts',(1.68439754047449,2.91666666666666,-0.972487373415292));
#20170=CARTESIAN_POINT('Ctrl Pts',(2.24586338729932,2.97499999999999,-4.12558411286752E-16));
#20171=CARTESIAN_POINT('Ctrl Pts',(1.68439754047449,3.03333333333333,0.97248737341529));
#20172=CARTESIAN_POINT('Ctrl Pts',(1.12293169364966,3.09166666666666,1.94497474683058));
#20173=CARTESIAN_POINT('Ctrl Pts',(0.,3.14999999999999,1.94497474683058));
#20174=CARTESIAN_POINT('Ctrl Pts',(-1.12293169364966,3.20833333333333,1.94497474683058));
#20175=CARTESIAN_POINT('Ctrl Pts',(-1.68439754047449,3.26666666666666,0.972487373415292));
#20176=CARTESIAN_POINT('Ctrl Pts',(-2.24586338729932,3.32499999999999,1.37519470428917E-16));
#20177=CARTESIAN_POINT('Ctrl Pts',(-1.68439754047449,3.38333333333333,-0.972487373415291));
#20178=CARTESIAN_POINT('Ctrl Pts',(-1.12293169364966,3.44166666666666,-1.94497474683058));
#20179=CARTESIAN_POINT('Ctrl Pts',(-2.38190709812851E-16,3.49999999999999,
-1.94497474683058));
#20180=CARTESIAN_POINT('Ctrl Pts',(1.12293169364966,3.55833333333333,-1.94497474683058));
#20181=CARTESIAN_POINT('Ctrl Pts',(1.68439754047449,3.61666666666666,-0.972487373415292));
#20182=CARTESIAN_POINT('Ctrl Pts',(2.24586338729932,3.67499999999999,-4.12558411286752E-16));
#20183=CARTESIAN_POINT('Ctrl Pts',(1.68439754047449,3.73333333333332,0.97248737341529));
#20184=CARTESIAN_POINT('Ctrl Pts',(1.12293169364966,3.79166666666666,1.94497474683058));
#20185=CARTESIAN_POINT('Ctrl Pts',(0.,3.84999999999999,1.94497474683058));
#20186=CARTESIAN_POINT('Ctrl Pts',(0.,-0.205025253169417,1.8));
#20187=CARTESIAN_POINT('Ctrl Pts',(-1.03923048454133,-0.146691919836083,
1.8));
#20188=CARTESIAN_POINT('Ctrl Pts',(-1.55884572681199,-0.0883585865027503,
0.9));
#20189=CARTESIAN_POINT('Ctrl Pts',(-2.07846096908265,-0.0300252531694171,
1.27269028646989E-16));
#20190=CARTESIAN_POINT('Ctrl Pts',(-1.55884572681199,0.0283080801639161,
-0.9));
#20191=CARTESIAN_POINT('Ctrl Pts',(-1.03923048454133,0.0866414134972494,
-1.8));
#20192=CARTESIAN_POINT('Ctrl Pts',(-2.20436423846524E-16,0.144974746830583,
-1.8));
#20193=CARTESIAN_POINT('Ctrl Pts',(1.03923048454133,0.203308080163916,-1.8));
#20194=CARTESIAN_POINT('Ctrl Pts',(1.55884572681199,0.261641413497249,-0.900000000000001));
#20195=CARTESIAN_POINT('Ctrl Pts',(2.07846096908265,0.319974746830582,-3.81807085940967E-16));
#20196=CARTESIAN_POINT('Ctrl Pts',(1.55884572681199,0.378308080163915,0.899999999999999));
#20197=CARTESIAN_POINT('Ctrl Pts',(1.03923048454133,0.436641413497249,1.8));
#20198=CARTESIAN_POINT('Ctrl Pts',(0.,0.494974746830582,1.8));
#20199=CARTESIAN_POINT('Ctrl Pts',(-1.03923048454133,0.553308080163915,
1.8));
#20200=CARTESIAN_POINT('Ctrl Pts',(-1.55884572681199,0.611641413497248,
0.9));
#20201=CARTESIAN_POINT('Ctrl Pts',(-2.07846096908265,0.669974746830582,
1.27269028646989E-16));
#20202=CARTESIAN_POINT('Ctrl Pts',(-1.55884572681199,0.728308080163915,
-0.9));
#20203=CARTESIAN_POINT('Ctrl Pts',(-1.03923048454133,0.786641413497248,
-1.8));
#20204=CARTESIAN_POINT('Ctrl Pts',(-2.20436423846524E-16,0.844974746830581,
-1.8));
#20205=CARTESIAN_POINT('Ctrl Pts',(1.03923048454133,0.903308080163914,-1.8));
#20206=CARTESIAN_POINT('Ctrl Pts',(1.55884572681199,0.961641413497248,-0.900000000000001));
#20207=CARTESIAN_POINT('Ctrl Pts',(2.07846096908265,1.01997474683058,-3.81807085940967E-16));
#20208=CARTESIAN_POINT('Ctrl Pts',(1.55884572681199,1.07830808016391,0.899999999999999));
#20209=CARTESIAN_POINT('Ctrl Pts',(1.03923048454133,1.13664141349725,1.8));
#20210=CARTESIAN_POINT('Ctrl Pts',(0.,1.19497474683058,1.8));
#20211=CARTESIAN_POINT('Ctrl Pts',(-1.03923048454133,1.25330808016391,1.8));
#20212=CARTESIAN_POINT('Ctrl Pts',(-1.55884572681199,1.31164141349725,0.9));
#20213=CARTESIAN_POINT('Ctrl Pts',(-2.07846096908265,1.36997474683058,1.27269028646989E-16));
#20214=CARTESIAN_POINT('Ctrl Pts',(-1.55884572681199,1.42830808016391,-0.9));
#20215=CARTESIAN_POINT('Ctrl Pts',(-1.03923048454133,1.48664141349725,-1.8));
#20216=CARTESIAN_POINT('Ctrl Pts',(-2.20436423846524E-16,1.54497474683058,
-1.8));
#20217=CARTESIAN_POINT('Ctrl Pts',(1.03923048454133,1.60330808016391,-1.8));
#20218=CARTESIAN_POINT('Ctrl Pts',(1.55884572681199,1.66164141349725,-0.900000000000001));
#20219=CARTESIAN_POINT('Ctrl Pts',(2.07846096908265,1.71997474683058,-3.81807085940967E-16));
#20220=CARTESIAN_POINT('Ctrl Pts',(1.55884572681199,1.77830808016391,0.899999999999999));
#20221=CARTESIAN_POINT('Ctrl Pts',(1.03923048454133,1.83664141349725,1.8));
#20222=CARTESIAN_POINT('Ctrl Pts',(0.,1.89497474683058,1.8));
#20223=CARTESIAN_POINT('Ctrl Pts',(-1.03923048454133,1.95330808016391,1.8));
#20224=CARTESIAN_POINT('Ctrl Pts',(-1.55884572681199,2.01164141349725,0.9));
#20225=CARTESIAN_POINT('Ctrl Pts',(-2.07846096908265,2.06997474683058,1.27269028646989E-16));
#20226=CARTESIAN_POINT('Ctrl Pts',(-1.55884572681199,2.12830808016391,-0.9));
#20227=CARTESIAN_POINT('Ctrl Pts',(-1.03923048454133,2.18664141349725,-1.8));
#20228=CARTESIAN_POINT('Ctrl Pts',(-2.20436423846524E-16,2.24497474683058,
-1.8));
#20229=CARTESIAN_POINT('Ctrl Pts',(1.03923048454133,2.30330808016391,-1.8));
#20230=CARTESIAN_POINT('Ctrl Pts',(1.55884572681199,2.36164141349724,-0.900000000000001));
#20231=CARTESIAN_POINT('Ctrl Pts',(2.07846096908265,2.41997474683058,-3.81807085940967E-16));
#20232=CARTESIAN_POINT('Ctrl Pts',(1.55884572681199,2.47830808016391,0.899999999999999));
#20233=CARTESIAN_POINT('Ctrl Pts',(1.03923048454133,2.53664141349724,1.8));
#20234=CARTESIAN_POINT('Ctrl Pts',(0.,2.59497474683058,1.8));
#20235=CARTESIAN_POINT('Ctrl Pts',(-1.03923048454133,2.65330808016391,1.8));
#20236=CARTESIAN_POINT('Ctrl Pts',(-1.55884572681199,2.71164141349724,0.9));
#20237=CARTESIAN_POINT('Ctrl Pts',(-2.07846096908265,2.76997474683058,1.27269028646989E-16));
#20238=CARTESIAN_POINT('Ctrl Pts',(-1.55884572681199,2.82830808016391,-0.9));
#20239=CARTESIAN_POINT('Ctrl Pts',(-1.03923048454133,2.88664141349724,-1.8));
#20240=CARTESIAN_POINT('Ctrl Pts',(-2.20436423846524E-16,2.94497474683058,
-1.8));
#20241=CARTESIAN_POINT('Ctrl Pts',(1.03923048454133,3.00330808016391,-1.8));
#20242=CARTESIAN_POINT('Ctrl Pts',(1.55884572681199,3.06164141349724,-0.900000000000001));
#20243=CARTESIAN_POINT('Ctrl Pts',(2.07846096908265,3.11997474683058,-3.81807085940967E-16));
#20244=CARTESIAN_POINT('Ctrl Pts',(1.55884572681199,3.17830808016391,0.899999999999999));
#20245=CARTESIAN_POINT('Ctrl Pts',(1.03923048454133,3.23664141349724,1.8));
#20246=CARTESIAN_POINT('Ctrl Pts',(0.,3.29497474683058,1.8));
#20247=CARTESIAN_POINT('Ctrl Pts',(-1.03923048454133,3.35330808016391,1.8));
#20248=CARTESIAN_POINT('Ctrl Pts',(-1.55884572681199,3.41164141349724,0.9));
#20249=CARTESIAN_POINT('Ctrl Pts',(-2.07846096908265,3.46997474683058,1.27269028646989E-16));
#20250=CARTESIAN_POINT('Ctrl Pts',(-1.55884572681199,3.52830808016391,-0.9));
#20251=CARTESIAN_POINT('Ctrl Pts',(-1.03923048454133,3.58664141349724,-1.8));
#20252=CARTESIAN_POINT('Ctrl Pts',(-2.20436423846524E-16,3.64497474683058,
-1.8));
#20253=CARTESIAN_POINT('Ctrl Pts',(1.03923048454133,3.70330808016391,-1.8));
#20254=CARTESIAN_POINT('Ctrl Pts',(1.55884572681199,3.76164141349724,-0.900000000000001));
#20255=CARTESIAN_POINT('Ctrl Pts',(2.07846096908265,3.81997474683058,-3.81807085940967E-16));
#20256=CARTESIAN_POINT('Ctrl Pts',(1.55884572681199,3.87830808016391,0.899999999999999));
#20257=CARTESIAN_POINT('Ctrl Pts',(1.03923048454133,3.93664141349724,1.8));
#20258=CARTESIAN_POINT('Ctrl Pts',(0.,3.99497474683058,1.8));
#20259=CARTESIAN_POINT('Ctrl Pts',(0.,0.,1.8));
#20260=CARTESIAN_POINT('Ctrl Pts',(-1.03923048454133,0.0583333333333332,
1.8));
#20261=CARTESIAN_POINT('Ctrl Pts',(-1.55884572681199,0.116666666666666,
0.9));
#20262=CARTESIAN_POINT('Ctrl Pts',(-2.07846096908265,0.175,1.27269028646989E-16));
#20263=CARTESIAN_POINT('Ctrl Pts',(-1.55884572681199,0.233333333333333,
-0.9));
#20264=CARTESIAN_POINT('Ctrl Pts',(-1.03923048454133,0.291666666666666,
-1.8));
#20265=CARTESIAN_POINT('Ctrl Pts',(-2.20436423846524E-16,0.349999999999999,
-1.8));
#20266=CARTESIAN_POINT('Ctrl Pts',(1.03923048454133,0.408333333333333,-1.8));
#20267=CARTESIAN_POINT('Ctrl Pts',(1.55884572681199,0.466666666666666,-0.900000000000001));
#20268=CARTESIAN_POINT('Ctrl Pts',(2.07846096908265,0.524999999999999,-3.81807085940967E-16));
#20269=CARTESIAN_POINT('Ctrl Pts',(1.55884572681199,0.583333333333332,0.899999999999999));
#20270=CARTESIAN_POINT('Ctrl Pts',(1.03923048454133,0.641666666666665,1.8));
#20271=CARTESIAN_POINT('Ctrl Pts',(0.,0.699999999999999,1.8));
#20272=CARTESIAN_POINT('Ctrl Pts',(-1.03923048454133,0.758333333333332,
1.8));
#20273=CARTESIAN_POINT('Ctrl Pts',(-1.55884572681199,0.816666666666665,
0.9));
#20274=CARTESIAN_POINT('Ctrl Pts',(-2.07846096908265,0.874999999999998,
1.27269028646989E-16));
#20275=CARTESIAN_POINT('Ctrl Pts',(-1.55884572681199,0.933333333333332,
-0.9));
#20276=CARTESIAN_POINT('Ctrl Pts',(-1.03923048454133,0.991666666666665,
-1.8));
#20277=CARTESIAN_POINT('Ctrl Pts',(-2.20436423846524E-16,1.05,-1.8));
#20278=CARTESIAN_POINT('Ctrl Pts',(1.03923048454133,1.10833333333333,-1.8));
#20279=CARTESIAN_POINT('Ctrl Pts',(1.55884572681199,1.16666666666666,-0.900000000000001));
#20280=CARTESIAN_POINT('Ctrl Pts',(2.07846096908265,1.225,-3.81807085940967E-16));
#20281=CARTESIAN_POINT('Ctrl Pts',(1.55884572681199,1.28333333333333,0.899999999999999));
#20282=CARTESIAN_POINT('Ctrl Pts',(1.03923048454133,1.34166666666666,1.8));
#20283=CARTESIAN_POINT('Ctrl Pts',(0.,1.4,1.8));
#20284=CARTESIAN_POINT('Ctrl Pts',(-1.03923048454133,1.45833333333333,1.8));
#20285=CARTESIAN_POINT('Ctrl Pts',(-1.55884572681199,1.51666666666666,0.9));
#20286=CARTESIAN_POINT('Ctrl Pts',(-2.07846096908265,1.575,1.27269028646989E-16));
#20287=CARTESIAN_POINT('Ctrl Pts',(-1.55884572681199,1.63333333333333,-0.9));
#20288=CARTESIAN_POINT('Ctrl Pts',(-1.03923048454133,1.69166666666666,-1.8));
#20289=CARTESIAN_POINT('Ctrl Pts',(-2.20436423846524E-16,1.75,-1.8));
#20290=CARTESIAN_POINT('Ctrl Pts',(1.03923048454133,1.80833333333333,-1.8));
#20291=CARTESIAN_POINT('Ctrl Pts',(1.55884572681199,1.86666666666666,-0.900000000000001));
#20292=CARTESIAN_POINT('Ctrl Pts',(2.07846096908265,1.925,-3.81807085940967E-16));
#20293=CARTESIAN_POINT('Ctrl Pts',(1.55884572681199,1.98333333333333,0.899999999999999));
#20294=CARTESIAN_POINT('Ctrl Pts',(1.03923048454133,2.04166666666666,1.8));
#20295=CARTESIAN_POINT('Ctrl Pts',(0.,2.1,1.8));
#20296=CARTESIAN_POINT('Ctrl Pts',(-1.03923048454133,2.15833333333333,1.8));
#20297=CARTESIAN_POINT('Ctrl Pts',(-1.55884572681199,2.21666666666666,0.9));
#20298=CARTESIAN_POINT('Ctrl Pts',(-2.07846096908265,2.275,1.27269028646989E-16));
#20299=CARTESIAN_POINT('Ctrl Pts',(-1.55884572681199,2.33333333333333,-0.9));
#20300=CARTESIAN_POINT('Ctrl Pts',(-1.03923048454133,2.39166666666666,-1.8));
#20301=CARTESIAN_POINT('Ctrl Pts',(-2.20436423846524E-16,2.45,-1.8));
#20302=CARTESIAN_POINT('Ctrl Pts',(1.03923048454133,2.50833333333333,-1.8));
#20303=CARTESIAN_POINT('Ctrl Pts',(1.55884572681199,2.56666666666666,-0.900000000000001));
#20304=CARTESIAN_POINT('Ctrl Pts',(2.07846096908265,2.62499999999999,-3.81807085940967E-16));
#20305=CARTESIAN_POINT('Ctrl Pts',(1.55884572681199,2.68333333333333,0.899999999999999));
#20306=CARTESIAN_POINT('Ctrl Pts',(1.03923048454133,2.74166666666666,1.8));
#20307=CARTESIAN_POINT('Ctrl Pts',(0.,2.79999999999999,1.8));
#20308=CARTESIAN_POINT('Ctrl Pts',(-1.03923048454133,2.85833333333333,1.8));
#20309=CARTESIAN_POINT('Ctrl Pts',(-1.55884572681199,2.91666666666666,0.9));
#20310=CARTESIAN_POINT('Ctrl Pts',(-2.07846096908265,2.97499999999999,1.27269028646989E-16));
#20311=CARTESIAN_POINT('Ctrl Pts',(-1.55884572681199,3.03333333333333,-0.9));
#20312=CARTESIAN_POINT('Ctrl Pts',(-1.03923048454133,3.09166666666666,-1.8));
#20313=CARTESIAN_POINT('Ctrl Pts',(-2.20436423846524E-16,3.14999999999999,
-1.8));
#20314=CARTESIAN_POINT('Ctrl Pts',(1.03923048454133,3.20833333333333,-1.8));
#20315=CARTESIAN_POINT('Ctrl Pts',(1.55884572681199,3.26666666666666,-0.900000000000001));
#20316=CARTESIAN_POINT('Ctrl Pts',(2.07846096908265,3.32499999999999,-3.81807085940967E-16));
#20317=CARTESIAN_POINT('Ctrl Pts',(1.55884572681199,3.38333333333333,0.899999999999999));
#20318=CARTESIAN_POINT('Ctrl Pts',(1.03923048454133,3.44166666666666,1.8));
#20319=CARTESIAN_POINT('Ctrl Pts',(0.,3.49999999999999,1.8));
#20320=CARTESIAN_POINT('Ctrl Pts',(-1.03923048454133,3.55833333333333,1.8));
#20321=CARTESIAN_POINT('Ctrl Pts',(-1.55884572681199,3.61666666666666,0.9));
#20322=CARTESIAN_POINT('Ctrl Pts',(-2.07846096908265,3.67499999999999,1.27269028646989E-16));
#20323=CARTESIAN_POINT('Ctrl Pts',(-1.55884572681199,3.73333333333333,-0.9));
#20324=CARTESIAN_POINT('Ctrl Pts',(-1.03923048454133,3.79166666666666,-1.8));
#20325=CARTESIAN_POINT('Ctrl Pts',(-2.20436423846524E-16,3.84999999999999,
-1.8));
#20326=CARTESIAN_POINT('Ctrl Pts',(1.03923048454133,3.90833333333333,-1.8));
#20327=CARTESIAN_POINT('Ctrl Pts',(1.55884572681199,3.96666666666666,-0.900000000000001));
#20328=CARTESIAN_POINT('Ctrl Pts',(2.07846096908265,4.02499999999999,-3.81807085940967E-16));
#20329=CARTESIAN_POINT('Ctrl Pts',(1.55884572681199,4.08333333333333,0.899999999999999));
#20330=CARTESIAN_POINT('Ctrl Pts',(1.03923048454133,4.14166666666666,1.8));
#20331=CARTESIAN_POINT('Ctrl Pts',(0.,4.19999999999999,1.8));
#20332=CARTESIAN_POINT('',(-2.63299061816681E-16,-0.349999999999999,2.15));
#20333=CARTESIAN_POINT('Origin',(0.,0.,2.15));
#20334=CARTESIAN_POINT('Ctrl Pts',(-2.63299061816681E-16,-0.349999999999999,
2.15));
#20335=CARTESIAN_POINT('Ctrl Pts',(-1.2413030787577,-0.291666666666666,
2.15));
#20336=CARTESIAN_POINT('Ctrl Pts',(-1.86195461813654,-0.233333333333333,
1.075));
#20337=CARTESIAN_POINT('Ctrl Pts',(-2.48260615751539,-0.175,-1.52015784217237E-16));
#20338=CARTESIAN_POINT('Ctrl Pts',(-1.86195461813654,-0.116666666666666,
-1.075));
#20339=CARTESIAN_POINT('Ctrl Pts',(-1.2413030787577,-0.0583333333333332,
-2.15));
#20340=CARTESIAN_POINT('Ctrl Pts',(0.,0.,-2.15));
#20341=CARTESIAN_POINT('Ctrl Pts',(1.24130307875769,0.0583333333333333,
-2.15));
#20342=CARTESIAN_POINT('Ctrl Pts',(1.86195461813654,0.116666666666666,-1.075));
#20343=CARTESIAN_POINT('Ctrl Pts',(2.48260615751539,0.175,-1.52015784217237E-16));
#20344=CARTESIAN_POINT('Ctrl Pts',(1.86195461813654,0.233333333333333,1.075));
#20345=CARTESIAN_POINT('Ctrl Pts',(1.2413030787577,0.291666666666666,2.15));
#20346=CARTESIAN_POINT('Ctrl Pts',(2.63299061816681E-16,0.349999999999999,
2.15));
#20347=CARTESIAN_POINT('Ctrl Pts',(2.63299061816681E-16,0.349999999999999,
2.15));
#20348=CARTESIAN_POINT('Ctrl Pts',(-1.24130307875769,0.408333333333333,
2.15));
#20349=CARTESIAN_POINT('Ctrl Pts',(-1.86195461813654,0.466666666666666,
1.075));
#20350=CARTESIAN_POINT('Ctrl Pts',(-2.48260615751539,0.524999999999999,
4.5604735265171E-16));
#20351=CARTESIAN_POINT('Ctrl Pts',(-1.86195461813654,0.583333333333332,
-1.075));
#20352=CARTESIAN_POINT('Ctrl Pts',(-1.2413030787577,0.641666666666665,-2.15));
#20353=CARTESIAN_POINT('Ctrl Pts',(-5.26598123633362E-16,0.699999999999999,
-2.15));
#20354=CARTESIAN_POINT('Ctrl Pts',(1.24130307875769,0.758333333333332,-2.15));
#20355=CARTESIAN_POINT('Ctrl Pts',(1.86195461813654,0.816666666666665,-1.075));
#20356=CARTESIAN_POINT('Ctrl Pts',(2.48260615751539,0.874999999999999,-7.60078921086183E-16));
#20357=CARTESIAN_POINT('Ctrl Pts',(1.86195461813654,0.933333333333332,1.075));
#20358=CARTESIAN_POINT('Ctrl Pts',(1.2413030787577,0.991666666666665,2.15));
#20359=CARTESIAN_POINT('Ctrl Pts',(7.89897185450043E-16,1.05,2.15));
#20360=CARTESIAN_POINT('Ctrl Pts',(-1.24130307875769,1.10833333333333,2.15));
#20361=CARTESIAN_POINT('Ctrl Pts',(-1.86195461813654,1.16666666666666,1.075));
#20362=CARTESIAN_POINT('Ctrl Pts',(-2.48260615751539,1.225,3.26910770324048E-15));
#20363=CARTESIAN_POINT('Ctrl Pts',(-1.86195461813654,1.28333333333333,-1.075));
#20364=CARTESIAN_POINT('Ctrl Pts',(-1.2413030787577,1.34166666666666,-2.15));
#20365=CARTESIAN_POINT('Ctrl Pts',(-1.05319624726672E-15,1.4,-2.15));
#20366=CARTESIAN_POINT('Ctrl Pts',(1.24130307875769,1.45833333333333,-2.15));
#20367=CARTESIAN_POINT('Ctrl Pts',(1.86195461813654,1.51666666666666,-1.075));
#20368=CARTESIAN_POINT('Ctrl Pts',(2.48260615751539,1.575,-1.36814205795513E-15));
#20369=CARTESIAN_POINT('Ctrl Pts',(1.86195461813654,1.63333333333333,1.075));
#20370=CARTESIAN_POINT('Ctrl Pts',(1.2413030787577,1.69166666666666,2.15));
#20371=CARTESIAN_POINT('Ctrl Pts',(1.3164953090834E-15,1.75,2.15));
#20372=CARTESIAN_POINT('Ctrl Pts',(-1.24130307875769,1.80833333333333,2.15));
#20373=CARTESIAN_POINT('Ctrl Pts',(-1.86195461813654,1.86666666666666,1.075));
#20374=CARTESIAN_POINT('Ctrl Pts',(-2.48260615751539,1.925,6.08216805382924E-15));
#20375=CARTESIAN_POINT('Ctrl Pts',(-1.86195461813654,1.98333333333333,-1.075));
#20376=CARTESIAN_POINT('Ctrl Pts',(-1.2413030787577,2.04166666666666,-2.15));
#20377=CARTESIAN_POINT('Ctrl Pts',(-5.39896157561062E-15,2.1,-2.15));
#20378=CARTESIAN_POINT('Ctrl Pts',(1.24130307875769,2.15833333333333,-2.15));
#20379=CARTESIAN_POINT('Ctrl Pts',(1.86195461813654,2.21666666666666,-1.075));
#20380=CARTESIAN_POINT('Ctrl Pts',(2.48260615751539,2.275,-6.38619962226372E-15));
#20381=CARTESIAN_POINT('Ctrl Pts',(1.86195461813655,2.33333333333333,1.07499999999999));
#20382=CARTESIAN_POINT('Ctrl Pts',(1.2413030787577,2.39166666666666,2.15));
#20383=CARTESIAN_POINT('Ctrl Pts',(1.84309343271677E-15,2.45,2.15));
#20384=CARTESIAN_POINT('Ctrl Pts',(-1.24130307875769,2.50833333333333,2.15));
#20385=CARTESIAN_POINT('Ctrl Pts',(-1.86195461813654,2.56666666666666,1.075));
#20386=CARTESIAN_POINT('Ctrl Pts',(-2.48260615751539,2.62499999999999,6.69023119069819E-15));
#20387=CARTESIAN_POINT('Ctrl Pts',(-1.86195461813655,2.68333333333333,-1.07499999999999));
#20388=CARTESIAN_POINT('Ctrl Pts',(-1.2413030787577,2.74166666666666,-2.14999999999999));
#20389=CARTESIAN_POINT('Ctrl Pts',(-2.10639249453345E-15,2.79999999999999,
-2.15));
#20390=CARTESIAN_POINT('Ctrl Pts',(1.24130307875769,2.85833333333333,-2.15));
#20391=CARTESIAN_POINT('Ctrl Pts',(1.86195461813654,2.91666666666666,-1.075));
#20392=CARTESIAN_POINT('Ctrl Pts',(2.48260615751539,2.97499999999999,-6.99426275913266E-15));
#20393=CARTESIAN_POINT('Ctrl Pts',(1.86195461813655,3.03333333333333,1.07499999999999));
#20394=CARTESIAN_POINT('Ctrl Pts',(1.2413030787577,3.09166666666666,2.14999999999999));
#20395=CARTESIAN_POINT('Ctrl Pts',(2.36969155635013E-15,3.14999999999999,
2.15));
#20396=CARTESIAN_POINT('Ctrl Pts',(-1.24130307875769,3.20833333333333,2.15));
#20397=CARTESIAN_POINT('Ctrl Pts',(-1.86195461813654,3.26666666666666,1.075));
#20398=CARTESIAN_POINT('Ctrl Pts',(-2.48260615751539,3.32499999999999,7.29829432756713E-15));
#20399=CARTESIAN_POINT('Ctrl Pts',(-1.86195461813655,3.38333333333333,-1.07499999999999));
#20400=CARTESIAN_POINT('Ctrl Pts',(-1.2413030787577,3.44166666666666,-2.14999999999999));
#20401=CARTESIAN_POINT('Ctrl Pts',(-1.02713250275879E-14,3.49999999999999,
-2.15));
#20402=CARTESIAN_POINT('Ctrl Pts',(1.24130307875769,3.55833333333333,-2.15));
#20403=CARTESIAN_POINT('Ctrl Pts',(1.86195461813654,3.61666666666666,-1.075));
#20404=CARTESIAN_POINT('Ctrl Pts',(2.48260615751539,3.67499999999999,-7.60232589600161E-15));
#20405=CARTESIAN_POINT('Ctrl Pts',(1.86195461813655,3.73333333333333,1.07499999999999));
#20406=CARTESIAN_POINT('Ctrl Pts',(1.2413030787577,3.79166666666666,2.14999999999999));
#20407=CARTESIAN_POINT('Ctrl Pts',(1.05346240894046E-14,3.84999999999999,
2.15));
#20408=CARTESIAN_POINT('Origin',(-1.80160437084306E-13,4.2,2.15));
#20409=CARTESIAN_POINT('Ctrl Pts',(0.,4.28626379701574E-17,2.5));
#20410=CARTESIAN_POINT('Ctrl Pts',(-1.44337567297406,0.0583333333333333,
2.5));
#20411=CARTESIAN_POINT('Ctrl Pts',(-2.1650635094611,0.116666666666666,1.25));
#20412=CARTESIAN_POINT('Ctrl Pts',(-2.88675134594813,0.175,1.76762539787484E-16));
#20413=CARTESIAN_POINT('Ctrl Pts',(-2.1650635094611,0.233333333333333,-1.25));
#20414=CARTESIAN_POINT('Ctrl Pts',(-1.44337567297407,0.291666666666666,
-2.5));
#20415=CARTESIAN_POINT('Ctrl Pts',(-3.06161699786838E-16,0.349999999999999,
-2.5));
#20416=CARTESIAN_POINT('Ctrl Pts',(1.44337567297406,0.408333333333333,-2.5));
#20417=CARTESIAN_POINT('Ctrl Pts',(2.1650635094611,0.466666666666666,-1.25));
#20418=CARTESIAN_POINT('Ctrl Pts',(2.88675134594813,0.524999999999999,-5.30287619362453E-16));
#20419=CARTESIAN_POINT('Ctrl Pts',(2.1650635094611,0.583333333333332,1.25));
#20420=CARTESIAN_POINT('Ctrl Pts',(1.44337567297407,0.641666666666665,2.5));
#20421=CARTESIAN_POINT('Ctrl Pts',(0.,0.699999999999999,2.5));
#20422=CARTESIAN_POINT('Ctrl Pts',(-1.44337567297406,0.758333333333332,
2.5));
#20423=CARTESIAN_POINT('Ctrl Pts',(-2.1650635094611,0.816666666666665,1.25));
#20424=CARTESIAN_POINT('Ctrl Pts',(-2.88675134594813,0.874999999999998,
1.76762539787484E-16));
#20425=CARTESIAN_POINT('Ctrl Pts',(-2.1650635094611,0.933333333333332,-1.25));
#20426=CARTESIAN_POINT('Ctrl Pts',(-1.44337567297407,0.991666666666665,
-2.5));
#20427=CARTESIAN_POINT('Ctrl Pts',(-3.06161699786838E-16,1.05,-2.5));
#20428=CARTESIAN_POINT('Ctrl Pts',(1.44337567297406,1.10833333333333,-2.5));
#20429=CARTESIAN_POINT('Ctrl Pts',(2.1650635094611,1.16666666666666,-1.25));
#20430=CARTESIAN_POINT('Ctrl Pts',(2.88675134594813,1.225,-5.30287619362453E-16));
#20431=CARTESIAN_POINT('Ctrl Pts',(2.1650635094611,1.28333333333333,1.25));
#20432=CARTESIAN_POINT('Ctrl Pts',(1.44337567297407,1.34166666666666,2.5));
#20433=CARTESIAN_POINT('Ctrl Pts',(0.,1.4,2.5));
#20434=CARTESIAN_POINT('Ctrl Pts',(-1.44337567297406,1.45833333333333,2.5));
#20435=CARTESIAN_POINT('Ctrl Pts',(-2.1650635094611,1.51666666666666,1.25));
#20436=CARTESIAN_POINT('Ctrl Pts',(-2.88675134594813,1.575,1.76762539787484E-16));
#20437=CARTESIAN_POINT('Ctrl Pts',(-2.1650635094611,1.63333333333333,-1.25));
#20438=CARTESIAN_POINT('Ctrl Pts',(-1.44337567297407,1.69166666666666,-2.5));
#20439=CARTESIAN_POINT('Ctrl Pts',(-3.06161699786838E-16,1.75,-2.5));
#20440=CARTESIAN_POINT('Ctrl Pts',(1.44337567297406,1.80833333333333,-2.5));
#20441=CARTESIAN_POINT('Ctrl Pts',(2.1650635094611,1.86666666666666,-1.25));
#20442=CARTESIAN_POINT('Ctrl Pts',(2.88675134594813,1.925,-5.30287619362453E-16));
#20443=CARTESIAN_POINT('Ctrl Pts',(2.1650635094611,1.98333333333333,1.25));
#20444=CARTESIAN_POINT('Ctrl Pts',(1.44337567297407,2.04166666666666,2.5));
#20445=CARTESIAN_POINT('Ctrl Pts',(0.,2.1,2.5));
#20446=CARTESIAN_POINT('Ctrl Pts',(-1.44337567297406,2.15833333333333,2.5));
#20447=CARTESIAN_POINT('Ctrl Pts',(-2.1650635094611,2.21666666666666,1.25));
#20448=CARTESIAN_POINT('Ctrl Pts',(-2.88675134594813,2.275,1.76762539787484E-16));
#20449=CARTESIAN_POINT('Ctrl Pts',(-2.1650635094611,2.33333333333333,-1.25));
#20450=CARTESIAN_POINT('Ctrl Pts',(-1.44337567297407,2.39166666666666,-2.5));
#20451=CARTESIAN_POINT('Ctrl Pts',(-3.06161699786838E-16,2.45,-2.5));
#20452=CARTESIAN_POINT('Ctrl Pts',(1.44337567297406,2.50833333333333,-2.5));
#20453=CARTESIAN_POINT('Ctrl Pts',(2.1650635094611,2.56666666666666,-1.25));
#20454=CARTESIAN_POINT('Ctrl Pts',(2.88675134594813,2.62499999999999,-5.30287619362453E-16));
#20455=CARTESIAN_POINT('Ctrl Pts',(2.1650635094611,2.68333333333333,1.25));
#20456=CARTESIAN_POINT('Ctrl Pts',(1.44337567297407,2.74166666666666,2.5));
#20457=CARTESIAN_POINT('Ctrl Pts',(0.,2.79999999999999,2.5));
#20458=CARTESIAN_POINT('Ctrl Pts',(-1.44337567297406,2.85833333333333,2.5));
#20459=CARTESIAN_POINT('Ctrl Pts',(-2.1650635094611,2.91666666666666,1.25));
#20460=CARTESIAN_POINT('Ctrl Pts',(-2.88675134594813,2.97499999999999,1.76762539787484E-16));
#20461=CARTESIAN_POINT('Ctrl Pts',(-2.1650635094611,3.03333333333333,-1.25));
#20462=CARTESIAN_POINT('Ctrl Pts',(-1.44337567297407,3.09166666666666,-2.5));
#20463=CARTESIAN_POINT('Ctrl Pts',(-3.06161699786838E-16,3.14999999999999,
-2.5));
#20464=CARTESIAN_POINT('Ctrl Pts',(1.44337567297406,3.20833333333333,-2.5));
#20465=CARTESIAN_POINT('Ctrl Pts',(2.1650635094611,3.26666666666666,-1.25));
#20466=CARTESIAN_POINT('Ctrl Pts',(2.88675134594813,3.32499999999999,-5.30287619362453E-16));
#20467=CARTESIAN_POINT('Ctrl Pts',(2.1650635094611,3.38333333333333,1.25));
#20468=CARTESIAN_POINT('Ctrl Pts',(1.44337567297407,3.44166666666666,2.5));
#20469=CARTESIAN_POINT('Ctrl Pts',(0.,3.49999999999999,2.5));
#20470=CARTESIAN_POINT('Ctrl Pts',(-1.44337567297406,3.55833333333333,2.5));
#20471=CARTESIAN_POINT('Ctrl Pts',(-2.1650635094611,3.61666666666666,1.25));
#20472=CARTESIAN_POINT('Ctrl Pts',(-2.88675134594813,3.67499999999999,1.76762539787484E-16));
#20473=CARTESIAN_POINT('Ctrl Pts',(-2.1650635094611,3.73333333333333,-1.25));
#20474=CARTESIAN_POINT('Ctrl Pts',(-1.44337567297407,3.79166666666666,-2.5));
#20475=CARTESIAN_POINT('Ctrl Pts',(-3.06161699786838E-16,3.84999999999999,
-2.5));
#20476=CARTESIAN_POINT('Ctrl Pts',(1.44337567297406,3.90833333333333,-2.5));
#20477=CARTESIAN_POINT('Ctrl Pts',(2.1650635094611,3.96666666666666,-1.25));
#20478=CARTESIAN_POINT('Ctrl Pts',(2.88675134594813,4.02499999999999,-5.30287619362453E-16));
#20479=CARTESIAN_POINT('Ctrl Pts',(2.1650635094611,4.08333333333333,1.25));
#20480=CARTESIAN_POINT('Ctrl Pts',(1.44337567297407,4.14166666666666,2.5));
#20481=CARTESIAN_POINT('Ctrl Pts',(0.,4.19999999999999,2.5));
#20482=CARTESIAN_POINT('Ctrl Pts',(0.,-0.205025253169417,2.5));
#20483=CARTESIAN_POINT('Ctrl Pts',(-1.44337567297406,-0.146691919836083,
2.5));
#20484=CARTESIAN_POINT('Ctrl Pts',(-2.1650635094611,-0.0883585865027503,
1.25));
#20485=CARTESIAN_POINT('Ctrl Pts',(-2.88675134594813,-0.0300252531694171,
1.76762539787484E-16));
#20486=CARTESIAN_POINT('Ctrl Pts',(-2.1650635094611,0.0283080801639162,
-1.25));
#20487=CARTESIAN_POINT('Ctrl Pts',(-1.44337567297407,0.0866414134972494,
-2.5));
#20488=CARTESIAN_POINT('Ctrl Pts',(-3.06161699786838E-16,0.144974746830583,
-2.5));
#20489=CARTESIAN_POINT('Ctrl Pts',(1.44337567297406,0.203308080163916,-2.5));
#20490=CARTESIAN_POINT('Ctrl Pts',(2.1650635094611,0.261641413497249,-1.25));
#20491=CARTESIAN_POINT('Ctrl Pts',(2.88675134594813,0.319974746830582,-5.30287619362453E-16));
#20492=CARTESIAN_POINT('Ctrl Pts',(2.1650635094611,0.378308080163915,1.25));
#20493=CARTESIAN_POINT('Ctrl Pts',(1.44337567297407,0.436641413497249,2.5));
#20494=CARTESIAN_POINT('Ctrl Pts',(0.,0.494974746830582,2.5));
#20495=CARTESIAN_POINT('Ctrl Pts',(-1.44337567297406,0.553308080163915,
2.5));
#20496=CARTESIAN_POINT('Ctrl Pts',(-2.1650635094611,0.611641413497248,1.25));
#20497=CARTESIAN_POINT('Ctrl Pts',(-2.88675134594813,0.669974746830582,
1.76762539787484E-16));
#20498=CARTESIAN_POINT('Ctrl Pts',(-2.1650635094611,0.728308080163915,-1.25));
#20499=CARTESIAN_POINT('Ctrl Pts',(-1.44337567297407,0.786641413497248,
-2.5));
#20500=CARTESIAN_POINT('Ctrl Pts',(-3.06161699786838E-16,0.844974746830581,
-2.5));
#20501=CARTESIAN_POINT('Ctrl Pts',(1.44337567297406,0.903308080163914,-2.5));
#20502=CARTESIAN_POINT('Ctrl Pts',(2.1650635094611,0.961641413497248,-1.25));
#20503=CARTESIAN_POINT('Ctrl Pts',(2.88675134594813,1.01997474683058,-5.30287619362453E-16));
#20504=CARTESIAN_POINT('Ctrl Pts',(2.1650635094611,1.07830808016391,1.25));
#20505=CARTESIAN_POINT('Ctrl Pts',(1.44337567297407,1.13664141349725,2.5));
#20506=CARTESIAN_POINT('Ctrl Pts',(0.,1.19497474683058,2.5));
#20507=CARTESIAN_POINT('Ctrl Pts',(-1.44337567297406,1.25330808016391,2.5));
#20508=CARTESIAN_POINT('Ctrl Pts',(-2.1650635094611,1.31164141349725,1.25));
#20509=CARTESIAN_POINT('Ctrl Pts',(-2.88675134594813,1.36997474683058,1.76762539787484E-16));
#20510=CARTESIAN_POINT('Ctrl Pts',(-2.1650635094611,1.42830808016391,-1.25));
#20511=CARTESIAN_POINT('Ctrl Pts',(-1.44337567297407,1.48664141349725,-2.5));
#20512=CARTESIAN_POINT('Ctrl Pts',(-3.06161699786838E-16,1.54497474683058,
-2.5));
#20513=CARTESIAN_POINT('Ctrl Pts',(1.44337567297406,1.60330808016391,-2.5));
#20514=CARTESIAN_POINT('Ctrl Pts',(2.1650635094611,1.66164141349725,-1.25));
#20515=CARTESIAN_POINT('Ctrl Pts',(2.88675134594813,1.71997474683058,-5.30287619362453E-16));
#20516=CARTESIAN_POINT('Ctrl Pts',(2.1650635094611,1.77830808016391,1.25));
#20517=CARTESIAN_POINT('Ctrl Pts',(1.44337567297407,1.83664141349725,2.5));
#20518=CARTESIAN_POINT('Ctrl Pts',(0.,1.89497474683058,2.5));
#20519=CARTESIAN_POINT('Ctrl Pts',(-1.44337567297406,1.95330808016391,2.5));
#20520=CARTESIAN_POINT('Ctrl Pts',(-2.1650635094611,2.01164141349725,1.25));
#20521=CARTESIAN_POINT('Ctrl Pts',(-2.88675134594813,2.06997474683058,1.76762539787484E-16));
#20522=CARTESIAN_POINT('Ctrl Pts',(-2.1650635094611,2.12830808016391,-1.25));
#20523=CARTESIAN_POINT('Ctrl Pts',(-1.44337567297407,2.18664141349725,-2.5));
#20524=CARTESIAN_POINT('Ctrl Pts',(-3.06161699786838E-16,2.24497474683058,
-2.5));
#20525=CARTESIAN_POINT('Ctrl Pts',(1.44337567297406,2.30330808016391,-2.5));
#20526=CARTESIAN_POINT('Ctrl Pts',(2.1650635094611,2.36164141349724,-1.25));
#20527=CARTESIAN_POINT('Ctrl Pts',(2.88675134594813,2.41997474683058,-5.30287619362453E-16));
#20528=CARTESIAN_POINT('Ctrl Pts',(2.1650635094611,2.47830808016391,1.25));
#20529=CARTESIAN_POINT('Ctrl Pts',(1.44337567297407,2.53664141349724,2.5));
#20530=CARTESIAN_POINT('Ctrl Pts',(0.,2.59497474683058,2.5));
#20531=CARTESIAN_POINT('Ctrl Pts',(-1.44337567297406,2.65330808016391,2.5));
#20532=CARTESIAN_POINT('Ctrl Pts',(-2.1650635094611,2.71164141349724,1.25));
#20533=CARTESIAN_POINT('Ctrl Pts',(-2.88675134594813,2.76997474683058,1.76762539787484E-16));
#20534=CARTESIAN_POINT('Ctrl Pts',(-2.1650635094611,2.82830808016391,-1.25));
#20535=CARTESIAN_POINT('Ctrl Pts',(-1.44337567297407,2.88664141349724,-2.5));
#20536=CARTESIAN_POINT('Ctrl Pts',(-3.06161699786838E-16,2.94497474683058,
-2.5));
#20537=CARTESIAN_POINT('Ctrl Pts',(1.44337567297406,3.00330808016391,-2.5));
#20538=CARTESIAN_POINT('Ctrl Pts',(2.1650635094611,3.06164141349724,-1.25));
#20539=CARTESIAN_POINT('Ctrl Pts',(2.88675134594813,3.11997474683058,-5.30287619362453E-16));
#20540=CARTESIAN_POINT('Ctrl Pts',(2.1650635094611,3.17830808016391,1.25));
#20541=CARTESIAN_POINT('Ctrl Pts',(1.44337567297407,3.23664141349724,2.5));
#20542=CARTESIAN_POINT('Ctrl Pts',(0.,3.29497474683058,2.5));
#20543=CARTESIAN_POINT('Ctrl Pts',(-1.44337567297406,3.35330808016391,2.5));
#20544=CARTESIAN_POINT('Ctrl Pts',(-2.1650635094611,3.41164141349724,1.25));
#20545=CARTESIAN_POINT('Ctrl Pts',(-2.88675134594813,3.46997474683058,1.76762539787484E-16));
#20546=CARTESIAN_POINT('Ctrl Pts',(-2.1650635094611,3.52830808016391,-1.25));
#20547=CARTESIAN_POINT('Ctrl Pts',(-1.44337567297407,3.58664141349724,-2.5));
#20548=CARTESIAN_POINT('Ctrl Pts',(-3.06161699786838E-16,3.64497474683058,
-2.5));
#20549=CARTESIAN_POINT('Ctrl Pts',(1.44337567297406,3.70330808016391,-2.5));
#20550=CARTESIAN_POINT('Ctrl Pts',(2.1650635094611,3.76164141349724,-1.25));
#20551=CARTESIAN_POINT('Ctrl Pts',(2.88675134594813,3.81997474683058,-5.30287619362453E-16));
#20552=CARTESIAN_POINT('Ctrl Pts',(2.1650635094611,3.87830808016391,1.25));
#20553=CARTESIAN_POINT('Ctrl Pts',(1.44337567297407,3.93664141349724,2.5));
#20554=CARTESIAN_POINT('Ctrl Pts',(0.,3.99497474683058,2.5));
#20555=CARTESIAN_POINT('Ctrl Pts',(0.,-0.35,2.35502525316942));
#20556=CARTESIAN_POINT('Ctrl Pts',(-1.35967446386573,-0.291666666666667,
2.35502525316942));
#20557=CARTESIAN_POINT('Ctrl Pts',(-2.03951169579859,-0.233333333333334,
1.17751262658471));
#20558=CARTESIAN_POINT('Ctrl Pts',(-2.71934892773146,-0.175,1.66512098005556E-16));
#20559=CARTESIAN_POINT('Ctrl Pts',(-2.03951169579859,-0.116666666666667,
-1.17751262658471));
#20560=CARTESIAN_POINT('Ctrl Pts',(-1.35967446386573,-0.0583333333333339,
-2.35502525316942));
#20561=CARTESIAN_POINT('Ctrl Pts',(-2.88407413820511E-16,-7.04731412115578E-16,
-2.35502525316942));
#20562=CARTESIAN_POINT('Ctrl Pts',(1.35967446386573,0.0583333333333326,
-2.35502525316942));
#20563=CARTESIAN_POINT('Ctrl Pts',(2.03951169579859,0.116666666666666,-1.17751262658471));
#20564=CARTESIAN_POINT('Ctrl Pts',(2.71934892773146,0.174999999999999,-4.99536294016668E-16));
#20565=CARTESIAN_POINT('Ctrl Pts',(2.03951169579859,0.233333333333332,1.17751262658471));
#20566=CARTESIAN_POINT('Ctrl Pts',(1.35967446386573,0.291666666666665,2.35502525316942));
#20567=CARTESIAN_POINT('Ctrl Pts',(0.,0.349999999999999,2.35502525316942));
#20568=CARTESIAN_POINT('Ctrl Pts',(-1.35967446386573,0.408333333333332,
2.35502525316942));
#20569=CARTESIAN_POINT('Ctrl Pts',(-2.03951169579859,0.466666666666665,
1.17751262658471));
#20570=CARTESIAN_POINT('Ctrl Pts',(-2.71934892773146,0.524999999999998,
1.66512098005556E-16));
#20571=CARTESIAN_POINT('Ctrl Pts',(-2.03951169579859,0.583333333333332,
-1.17751262658471));
#20572=CARTESIAN_POINT('Ctrl Pts',(-1.35967446386573,0.641666666666665,
-2.35502525316942));
#20573=CARTESIAN_POINT('Ctrl Pts',(-2.88407413820511E-16,0.699999999999998,
-2.35502525316942));
#20574=CARTESIAN_POINT('Ctrl Pts',(1.35967446386573,0.758333333333331,-2.35502525316942));
#20575=CARTESIAN_POINT('Ctrl Pts',(2.03951169579859,0.816666666666664,-1.17751262658471));
#20576=CARTESIAN_POINT('Ctrl Pts',(2.71934892773146,0.874999999999998,-4.99536294016668E-16));
#20577=CARTESIAN_POINT('Ctrl Pts',(2.03951169579859,0.933333333333331,1.17751262658471));
#20578=CARTESIAN_POINT('Ctrl Pts',(1.35967446386573,0.991666666666664,2.35502525316942));
#20579=CARTESIAN_POINT('Ctrl Pts',(0.,1.05,2.35502525316942));
#20580=CARTESIAN_POINT('Ctrl Pts',(-1.35967446386573,1.10833333333333,2.35502525316942));
#20581=CARTESIAN_POINT('Ctrl Pts',(-2.03951169579859,1.16666666666666,1.17751262658471));
#20582=CARTESIAN_POINT('Ctrl Pts',(-2.71934892773146,1.225,1.66512098005556E-16));
#20583=CARTESIAN_POINT('Ctrl Pts',(-2.03951169579859,1.28333333333333,-1.17751262658471));
#20584=CARTESIAN_POINT('Ctrl Pts',(-1.35967446386573,1.34166666666666,-2.35502525316942));
#20585=CARTESIAN_POINT('Ctrl Pts',(-2.88407413820511E-16,1.4,-2.35502525316942));
#20586=CARTESIAN_POINT('Ctrl Pts',(1.35967446386573,1.45833333333333,-2.35502525316942));
#20587=CARTESIAN_POINT('Ctrl Pts',(2.03951169579859,1.51666666666666,-1.17751262658471));
#20588=CARTESIAN_POINT('Ctrl Pts',(2.71934892773146,1.575,-4.99536294016668E-16));
#20589=CARTESIAN_POINT('Ctrl Pts',(2.03951169579859,1.63333333333333,1.17751262658471));
#20590=CARTESIAN_POINT('Ctrl Pts',(1.35967446386573,1.69166666666666,2.35502525316942));
#20591=CARTESIAN_POINT('Ctrl Pts',(0.,1.75,2.35502525316942));
#20592=CARTESIAN_POINT('Ctrl Pts',(-1.35967446386573,1.80833333333333,2.35502525316942));
#20593=CARTESIAN_POINT('Ctrl Pts',(-2.03951169579859,1.86666666666666,1.17751262658471));
#20594=CARTESIAN_POINT('Ctrl Pts',(-2.71934892773146,1.925,1.66512098005556E-16));
#20595=CARTESIAN_POINT('Ctrl Pts',(-2.03951169579859,1.98333333333333,-1.17751262658471));
#20596=CARTESIAN_POINT('Ctrl Pts',(-1.35967446386573,2.04166666666666,-2.35502525316942));
#20597=CARTESIAN_POINT('Ctrl Pts',(-2.88407413820511E-16,2.09999999999999,
-2.35502525316942));
#20598=CARTESIAN_POINT('Ctrl Pts',(1.35967446386573,2.15833333333333,-2.35502525316942));
#20599=CARTESIAN_POINT('Ctrl Pts',(2.03951169579859,2.21666666666666,-1.17751262658471));
#20600=CARTESIAN_POINT('Ctrl Pts',(2.71934892773146,2.275,-4.99536294016668E-16));
#20601=CARTESIAN_POINT('Ctrl Pts',(2.03951169579859,2.33333333333333,1.17751262658471));
#20602=CARTESIAN_POINT('Ctrl Pts',(1.35967446386573,2.39166666666666,2.35502525316942));
#20603=CARTESIAN_POINT('Ctrl Pts',(0.,2.44999999999999,2.35502525316942));
#20604=CARTESIAN_POINT('Ctrl Pts',(-1.35967446386573,2.50833333333333,2.35502525316942));
#20605=CARTESIAN_POINT('Ctrl Pts',(-2.03951169579859,2.56666666666666,1.17751262658471));
#20606=CARTESIAN_POINT('Ctrl Pts',(-2.71934892773146,2.62499999999999,1.66512098005556E-16));
#20607=CARTESIAN_POINT('Ctrl Pts',(-2.03951169579859,2.68333333333333,-1.17751262658471));
#20608=CARTESIAN_POINT('Ctrl Pts',(-1.35967446386573,2.74166666666666,-2.35502525316942));
#20609=CARTESIAN_POINT('Ctrl Pts',(-2.88407413820511E-16,2.79999999999999,
-2.35502525316942));
#20610=CARTESIAN_POINT('Ctrl Pts',(1.35967446386573,2.85833333333333,-2.35502525316942));
#20611=CARTESIAN_POINT('Ctrl Pts',(2.03951169579859,2.91666666666666,-1.17751262658471));
#20612=CARTESIAN_POINT('Ctrl Pts',(2.71934892773146,2.97499999999999,-4.99536294016668E-16));
#20613=CARTESIAN_POINT('Ctrl Pts',(2.03951169579859,3.03333333333333,1.17751262658471));
#20614=CARTESIAN_POINT('Ctrl Pts',(1.35967446386573,3.09166666666666,2.35502525316942));
#20615=CARTESIAN_POINT('Ctrl Pts',(0.,3.14999999999999,2.35502525316942));
#20616=CARTESIAN_POINT('Ctrl Pts',(-1.35967446386573,3.20833333333333,2.35502525316942));
#20617=CARTESIAN_POINT('Ctrl Pts',(-2.03951169579859,3.26666666666666,1.17751262658471));
#20618=CARTESIAN_POINT('Ctrl Pts',(-2.71934892773146,3.32499999999999,1.66512098005556E-16));
#20619=CARTESIAN_POINT('Ctrl Pts',(-2.03951169579859,3.38333333333333,-1.17751262658471));
#20620=CARTESIAN_POINT('Ctrl Pts',(-1.35967446386573,3.44166666666666,-2.35502525316942));
#20621=CARTESIAN_POINT('Ctrl Pts',(-2.88407413820511E-16,3.49999999999999,
-2.35502525316942));
#20622=CARTESIAN_POINT('Ctrl Pts',(1.35967446386573,3.55833333333333,-2.35502525316942));
#20623=CARTESIAN_POINT('Ctrl Pts',(2.03951169579859,3.61666666666666,-1.17751262658471));
#20624=CARTESIAN_POINT('Ctrl Pts',(2.71934892773146,3.67499999999999,-4.99536294016668E-16));
#20625=CARTESIAN_POINT('Ctrl Pts',(2.03951169579859,3.73333333333332,1.17751262658471));
#20626=CARTESIAN_POINT('Ctrl Pts',(1.35967446386573,3.79166666666666,2.35502525316942));
#20627=CARTESIAN_POINT('Ctrl Pts',(0.,3.84999999999999,2.35502525316942));
#20628=CARTESIAN_POINT('Ctrl Pts',(0.,-0.35,2.15));
#20629=CARTESIAN_POINT('Ctrl Pts',(-1.2413030787577,-0.291666666666667,
2.15));
#20630=CARTESIAN_POINT('Ctrl Pts',(-1.86195461813654,-0.233333333333334,
1.075));
#20631=CARTESIAN_POINT('Ctrl Pts',(-2.48260615751539,-0.175,1.52015784217237E-16));
#20632=CARTESIAN_POINT('Ctrl Pts',(-1.86195461813654,-0.116666666666667,
-1.075));
#20633=CARTESIAN_POINT('Ctrl Pts',(-1.2413030787577,-0.058333333333334,
-2.15));
#20634=CARTESIAN_POINT('Ctrl Pts',(-2.63299061816681E-16,-7.58941520739853E-16,
-2.15));
#20635=CARTESIAN_POINT('Ctrl Pts',(1.24130307875769,0.0583333333333325,
-2.15));
#20636=CARTESIAN_POINT('Ctrl Pts',(1.86195461813654,0.116666666666666,-1.075));
#20637=CARTESIAN_POINT('Ctrl Pts',(2.48260615751539,0.174999999999999,-4.5604735265171E-16));
#20638=CARTESIAN_POINT('Ctrl Pts',(1.86195461813654,0.233333333333332,1.075));
#20639=CARTESIAN_POINT('Ctrl Pts',(1.2413030787577,0.291666666666665,2.15));
#20640=CARTESIAN_POINT('Ctrl Pts',(0.,0.349999999999999,2.15));
#20641=CARTESIAN_POINT('Ctrl Pts',(-1.2413030787577,0.408333333333332,2.15));
#20642=CARTESIAN_POINT('Ctrl Pts',(-1.86195461813654,0.466666666666665,
1.075));
#20643=CARTESIAN_POINT('Ctrl Pts',(-2.48260615751539,0.524999999999998,
1.52015784217237E-16));
#20644=CARTESIAN_POINT('Ctrl Pts',(-1.86195461813654,0.583333333333331,
-1.075));
#20645=CARTESIAN_POINT('Ctrl Pts',(-1.2413030787577,0.641666666666665,-2.15));
#20646=CARTESIAN_POINT('Ctrl Pts',(-2.63299061816681E-16,0.699999999999998,
-2.15));
#20647=CARTESIAN_POINT('Ctrl Pts',(1.24130307875769,0.758333333333331,-2.15));
#20648=CARTESIAN_POINT('Ctrl Pts',(1.86195461813654,0.816666666666664,-1.075));
#20649=CARTESIAN_POINT('Ctrl Pts',(2.48260615751539,0.874999999999997,-4.5604735265171E-16));
#20650=CARTESIAN_POINT('Ctrl Pts',(1.86195461813654,0.933333333333331,1.075));
#20651=CARTESIAN_POINT('Ctrl Pts',(1.2413030787577,0.991666666666664,2.15));
#20652=CARTESIAN_POINT('Ctrl Pts',(0.,1.05,2.15));
#20653=CARTESIAN_POINT('Ctrl Pts',(-1.2413030787577,1.10833333333333,2.15));
#20654=CARTESIAN_POINT('Ctrl Pts',(-1.86195461813654,1.16666666666666,1.075));
#20655=CARTESIAN_POINT('Ctrl Pts',(-2.48260615751539,1.225,1.52015784217237E-16));
#20656=CARTESIAN_POINT('Ctrl Pts',(-1.86195461813654,1.28333333333333,-1.075));
#20657=CARTESIAN_POINT('Ctrl Pts',(-1.2413030787577,1.34166666666666,-2.15));
#20658=CARTESIAN_POINT('Ctrl Pts',(-2.63299061816681E-16,1.4,-2.15));
#20659=CARTESIAN_POINT('Ctrl Pts',(1.24130307875769,1.45833333333333,-2.15));
#20660=CARTESIAN_POINT('Ctrl Pts',(1.86195461813654,1.51666666666666,-1.075));
#20661=CARTESIAN_POINT('Ctrl Pts',(2.48260615751539,1.575,-4.5604735265171E-16));
#20662=CARTESIAN_POINT('Ctrl Pts',(1.86195461813654,1.63333333333333,1.075));
#20663=CARTESIAN_POINT('Ctrl Pts',(1.2413030787577,1.69166666666666,2.15));
#20664=CARTESIAN_POINT('Ctrl Pts',(0.,1.75,2.15));
#20665=CARTESIAN_POINT('Ctrl Pts',(-1.2413030787577,1.80833333333333,2.15));
#20666=CARTESIAN_POINT('Ctrl Pts',(-1.86195461813654,1.86666666666666,1.075));
#20667=CARTESIAN_POINT('Ctrl Pts',(-2.48260615751539,1.925,1.52015784217237E-16));
#20668=CARTESIAN_POINT('Ctrl Pts',(-1.86195461813654,1.98333333333333,-1.075));
#20669=CARTESIAN_POINT('Ctrl Pts',(-1.2413030787577,2.04166666666666,-2.15));
#20670=CARTESIAN_POINT('Ctrl Pts',(-2.63299061816681E-16,2.1,-2.15));
#20671=CARTESIAN_POINT('Ctrl Pts',(1.24130307875769,2.15833333333333,-2.15));
#20672=CARTESIAN_POINT('Ctrl Pts',(1.86195461813654,2.21666666666666,-1.075));
#20673=CARTESIAN_POINT('Ctrl Pts',(2.48260615751539,2.275,-4.5604735265171E-16));
#20674=CARTESIAN_POINT('Ctrl Pts',(1.86195461813654,2.33333333333333,1.075));
#20675=CARTESIAN_POINT('Ctrl Pts',(1.2413030787577,2.39166666666666,2.15));
#20676=CARTESIAN_POINT('Ctrl Pts',(0.,2.44999999999999,2.15));
#20677=CARTESIAN_POINT('Ctrl Pts',(-1.2413030787577,2.50833333333333,2.15));
#20678=CARTESIAN_POINT('Ctrl Pts',(-1.86195461813654,2.56666666666666,1.075));
#20679=CARTESIAN_POINT('Ctrl Pts',(-2.48260615751539,2.62499999999999,1.52015784217237E-16));
#20680=CARTESIAN_POINT('Ctrl Pts',(-1.86195461813654,2.68333333333333,-1.075));
#20681=CARTESIAN_POINT('Ctrl Pts',(-1.2413030787577,2.74166666666666,-2.15));
#20682=CARTESIAN_POINT('Ctrl Pts',(-2.63299061816681E-16,2.79999999999999,
-2.15));
#20683=CARTESIAN_POINT('Ctrl Pts',(1.24130307875769,2.85833333333333,-2.15));
#20684=CARTESIAN_POINT('Ctrl Pts',(1.86195461813654,2.91666666666666,-1.075));
#20685=CARTESIAN_POINT('Ctrl Pts',(2.48260615751539,2.97499999999999,-4.5604735265171E-16));
#20686=CARTESIAN_POINT('Ctrl Pts',(1.86195461813654,3.03333333333333,1.075));
#20687=CARTESIAN_POINT('Ctrl Pts',(1.2413030787577,3.09166666666666,2.15));
#20688=CARTESIAN_POINT('Ctrl Pts',(0.,3.14999999999999,2.15));
#20689=CARTESIAN_POINT('Ctrl Pts',(-1.2413030787577,3.20833333333333,2.15));
#20690=CARTESIAN_POINT('Ctrl Pts',(-1.86195461813654,3.26666666666666,1.075));
#20691=CARTESIAN_POINT('Ctrl Pts',(-2.48260615751539,3.32499999999999,1.52015784217237E-16));
#20692=CARTESIAN_POINT('Ctrl Pts',(-1.86195461813654,3.38333333333333,-1.075));
#20693=CARTESIAN_POINT('Ctrl Pts',(-1.2413030787577,3.44166666666666,-2.15));
#20694=CARTESIAN_POINT('Ctrl Pts',(-2.63299061816681E-16,3.49999999999999,
-2.15));
#20695=CARTESIAN_POINT('Ctrl Pts',(1.24130307875769,3.55833333333333,-2.15));
#20696=CARTESIAN_POINT('Ctrl Pts',(1.86195461813654,3.61666666666666,-1.075));
#20697=CARTESIAN_POINT('Ctrl Pts',(2.48260615751539,3.67499999999999,-4.5604735265171E-16));
#20698=CARTESIAN_POINT('Ctrl Pts',(1.86195461813654,3.73333333333333,1.075));
#20699=CARTESIAN_POINT('Ctrl Pts',(1.2413030787577,3.79166666666666,2.15));
#20700=CARTESIAN_POINT('Ctrl Pts',(0.,3.84999999999999,2.15));
#20701=CARTESIAN_POINT('',(0.,4.28626379701574E-17,2.5));
#20702=CARTESIAN_POINT('Origin',(0.,0.,2.15));
#20703=CARTESIAN_POINT('',(-1.02907469966573E-13,4.2,2.5));
#20704=CARTESIAN_POINT('Ctrl Pts',(0.,4.28626379701574E-17,2.5));
#20705=CARTESIAN_POINT('Ctrl Pts',(-1.44337567297406,0.0583333333333333,
2.5));
#20706=CARTESIAN_POINT('Ctrl Pts',(-2.1650635094611,0.116666666666666,1.25));
#20707=CARTESIAN_POINT('Ctrl Pts',(-2.88675134594813,0.175,1.76762539787484E-16));
#20708=CARTESIAN_POINT('Ctrl Pts',(-2.1650635094611,0.233333333333333,-1.25));
#20709=CARTESIAN_POINT('Ctrl Pts',(-1.44337567297407,0.291666666666666,
-2.5));
#20710=CARTESIAN_POINT('Ctrl Pts',(-3.06161699786838E-16,0.349999999999999,
-2.5));
#20711=CARTESIAN_POINT('Ctrl Pts',(1.44337567297406,0.408333333333333,-2.5));
#20712=CARTESIAN_POINT('Ctrl Pts',(2.1650635094611,0.466666666666666,-1.25));
#20713=CARTESIAN_POINT('Ctrl Pts',(2.88675134594813,0.524999999999999,-5.30287619362453E-16));
#20714=CARTESIAN_POINT('Ctrl Pts',(2.1650635094611,0.583333333333332,1.25));
#20715=CARTESIAN_POINT('Ctrl Pts',(1.44337567297407,0.641666666666665,2.5));
#20716=CARTESIAN_POINT('Ctrl Pts',(6.12323399573677E-16,0.699999999999999,
2.5));
#20717=CARTESIAN_POINT('Ctrl Pts',(-1.44337567297406,0.758333333333332,
2.5));
#20718=CARTESIAN_POINT('Ctrl Pts',(-2.1650635094611,0.816666666666665,1.25));
#20719=CARTESIAN_POINT('Ctrl Pts',(-2.88675134594813,0.874999999999998,
3.44776294744884E-15));
#20720=CARTESIAN_POINT('Ctrl Pts',(-2.1650635094611,0.933333333333332,-1.25));
#20721=CARTESIAN_POINT('Ctrl Pts',(-1.44337567297407,0.991666666666665,
-2.5));
#20722=CARTESIAN_POINT('Ctrl Pts',(-9.18485099360515E-16,1.05,-2.5));
#20723=CARTESIAN_POINT('Ctrl Pts',(1.44337567297406,1.10833333333333,-2.5));
#20724=CARTESIAN_POINT('Ctrl Pts',(2.16506350946109,1.16666666666666,-1.25));
#20725=CARTESIAN_POINT('Ctrl Pts',(2.88675134594813,1.225,-1.23733777851239E-15));
#20726=CARTESIAN_POINT('Ctrl Pts',(2.1650635094611,1.28333333333333,1.25));
#20727=CARTESIAN_POINT('Ctrl Pts',(1.44337567297407,1.34166666666666,2.5));
#20728=CARTESIAN_POINT('Ctrl Pts',(1.22464679914735E-15,1.4,2.5));
#20729=CARTESIAN_POINT('Ctrl Pts',(-1.44337567297406,1.45833333333333,2.5));
#20730=CARTESIAN_POINT('Ctrl Pts',(-2.16506350946109,1.51666666666666,1.25));
#20731=CARTESIAN_POINT('Ctrl Pts',(-2.88675134594813,1.575,6.7187633551102E-15));
#20732=CARTESIAN_POINT('Ctrl Pts',(-2.1650635094611,1.63333333333333,-1.25));
#20733=CARTESIAN_POINT('Ctrl Pts',(-1.44337567297407,1.69166666666666,-2.5));
#20734=CARTESIAN_POINT('Ctrl Pts',(-5.97170059743482E-15,1.75,-2.5));
#20735=CARTESIAN_POINT('Ctrl Pts',(1.44337567297406,1.80833333333333,-2.5));
#20736=CARTESIAN_POINT('Ctrl Pts',(2.16506350946109,1.86666666666666,-1.25));
#20737=CARTESIAN_POINT('Ctrl Pts',(2.88675134594813,1.925,-7.07228843468517E-15));
#20738=CARTESIAN_POINT('Ctrl Pts',(2.1650635094611,1.98333333333333,1.24999999999999));
#20739=CARTESIAN_POINT('Ctrl Pts',(1.44337567297407,2.04166666666666,2.49999999999999));
#20740=CARTESIAN_POINT('Ctrl Pts',(1.83697019872103E-15,2.1,2.5));
#20741=CARTESIAN_POINT('Ctrl Pts',(-1.44337567297406,2.15833333333333,2.5));
#20742=CARTESIAN_POINT('Ctrl Pts',(-2.16506350946109,2.21666666666666,1.25));
#20743=CARTESIAN_POINT('Ctrl Pts',(-2.88675134594813,2.275,7.42581351426014E-15));
#20744=CARTESIAN_POINT('Ctrl Pts',(-2.1650635094611,2.33333333333333,-1.24999999999999));
#20745=CARTESIAN_POINT('Ctrl Pts',(-1.44337567297407,2.39166666666666,-2.49999999999999));
#20746=CARTESIAN_POINT('Ctrl Pts',(-2.14313189850787E-15,2.45,-2.5));
#20747=CARTESIAN_POINT('Ctrl Pts',(1.44337567297406,2.50833333333333,-2.5));
#20748=CARTESIAN_POINT('Ctrl Pts',(2.16506350946109,2.56666666666666,-1.25));
#20749=CARTESIAN_POINT('Ctrl Pts',(2.88675134594813,2.625,-7.7793385938351E-15));
#20750=CARTESIAN_POINT('Ctrl Pts',(2.1650635094611,2.68333333333333,1.24999999999999));
#20751=CARTESIAN_POINT('Ctrl Pts',(1.44337567297407,2.74166666666666,2.49999999999999));
#20752=CARTESIAN_POINT('Ctrl Pts',(2.44929359829471E-15,2.79999999999999,
2.5));
#20753=CARTESIAN_POINT('Ctrl Pts',(-1.44337567297406,2.85833333333333,2.5));
#20754=CARTESIAN_POINT('Ctrl Pts',(-2.16506350946109,2.91666666666666,1.25));
#20755=CARTESIAN_POINT('Ctrl Pts',(-2.88675134594813,2.97499999999999,8.13286367341007E-15));
#20756=CARTESIAN_POINT('Ctrl Pts',(-2.1650635094611,3.03333333333333,-1.24999999999999));
#20757=CARTESIAN_POINT('Ctrl Pts',(-1.44337567297407,3.09166666666666,-2.49999999999999));
#20758=CARTESIAN_POINT('Ctrl Pts',(-1.16372394950828E-14,3.14999999999999,
-2.5));
#20759=CARTESIAN_POINT('Ctrl Pts',(1.44337567297406,3.20833333333333,-2.5));
#20760=CARTESIAN_POINT('Ctrl Pts',(2.16506350946109,3.26666666666666,-1.25000000000001));
#20761=CARTESIAN_POINT('Ctrl Pts',(2.88675134594813,3.32499999999999,-8.48638875298504E-15));
#20762=CARTESIAN_POINT('Ctrl Pts',(2.1650635094611,3.38333333333333,1.24999999999999));
#20763=CARTESIAN_POINT('Ctrl Pts',(1.44337567297407,3.44166666666666,2.49999999999999));
#20764=CARTESIAN_POINT('Ctrl Pts',(1.19434011948696E-14,3.49999999999999,
2.5));
#20765=CARTESIAN_POINT('Ctrl Pts',(-1.44337567297406,3.55833333333333,2.5));
#20766=CARTESIAN_POINT('Ctrl Pts',(-2.16506350946109,3.61666666666666,1.25000000000001));
#20767=CARTESIAN_POINT('Ctrl Pts',(-2.88675134594813,3.67499999999999,1.90957148266057E-14));
#20768=CARTESIAN_POINT('Ctrl Pts',(-2.1650635094611,3.73333333333333,-1.24999999999999));
#20769=CARTESIAN_POINT('Ctrl Pts',(-1.44337567297407,3.79166666666666,-2.5));
#20770=CARTESIAN_POINT('Ctrl Pts',(-1.22495628946565E-14,3.84999999999999,
-2.5));
#20771=CARTESIAN_POINT('Ctrl Pts',(1.44337567297406,3.90833333333333,-2.5));
#20772=CARTESIAN_POINT('Ctrl Pts',(2.16506350946109,3.96666666666666,-1.25000000000001));
#20773=CARTESIAN_POINT('Ctrl Pts',(2.88675134594813,4.02499999999999,-9.19343891213498E-15));
#20774=CARTESIAN_POINT('Ctrl Pts',(2.16506350946111,4.08333333333333,1.24999999999998));
#20775=CARTESIAN_POINT('Ctrl Pts',(1.44337567297408,4.14166666666666,2.49999999999999));
#20776=CARTESIAN_POINT('Ctrl Pts',(-1.02907469966573E-13,4.2,2.5));
#20777=CARTESIAN_POINT('Origin',(-1.80160437084306E-13,4.2,2.15));
#20778=CARTESIAN_POINT('Ctrl Pts',(0.,0.35,2.15));
#20779=CARTESIAN_POINT('Ctrl Pts',(-1.2413030787577,0.408333333333333,2.15));
#20780=CARTESIAN_POINT('Ctrl Pts',(-1.86195461813654,0.466666666666667,
1.075));
#20781=CARTESIAN_POINT('Ctrl Pts',(-2.48260615751539,0.525,1.52015784217237E-16));
#20782=CARTESIAN_POINT('Ctrl Pts',(-1.86195461813654,0.583333333333333,
-1.075));
#20783=CARTESIAN_POINT('Ctrl Pts',(-1.2413030787577,0.641666666666666,-2.15));
#20784=CARTESIAN_POINT('Ctrl Pts',(-2.63299061816681E-16,0.699999999999999,
-2.15));
#20785=CARTESIAN_POINT('Ctrl Pts',(1.24130307875769,0.758333333333333,-2.15));
#20786=CARTESIAN_POINT('Ctrl Pts',(1.86195461813654,0.816666666666666,-1.075));
#20787=CARTESIAN_POINT('Ctrl Pts',(2.48260615751539,0.874999999999999,-4.5604735265171E-16));
#20788=CARTESIAN_POINT('Ctrl Pts',(1.86195461813654,0.933333333333332,1.075));
#20789=CARTESIAN_POINT('Ctrl Pts',(1.2413030787577,0.991666666666666,2.15));
#20790=CARTESIAN_POINT('Ctrl Pts',(0.,1.05,2.15));
#20791=CARTESIAN_POINT('Ctrl Pts',(-1.2413030787577,1.10833333333333,2.15));
#20792=CARTESIAN_POINT('Ctrl Pts',(-1.86195461813654,1.16666666666667,1.075));
#20793=CARTESIAN_POINT('Ctrl Pts',(-2.48260615751539,1.225,1.52015784217237E-16));
#20794=CARTESIAN_POINT('Ctrl Pts',(-1.86195461813654,1.28333333333333,-1.075));
#20795=CARTESIAN_POINT('Ctrl Pts',(-1.2413030787577,1.34166666666666,-2.15));
#20796=CARTESIAN_POINT('Ctrl Pts',(-2.63299061816681E-16,1.4,-2.15));
#20797=CARTESIAN_POINT('Ctrl Pts',(1.24130307875769,1.45833333333333,-2.15));
#20798=CARTESIAN_POINT('Ctrl Pts',(1.86195461813654,1.51666666666666,-1.075));
#20799=CARTESIAN_POINT('Ctrl Pts',(2.48260615751539,1.575,-4.5604735265171E-16));
#20800=CARTESIAN_POINT('Ctrl Pts',(1.86195461813654,1.63333333333333,1.075));
#20801=CARTESIAN_POINT('Ctrl Pts',(1.2413030787577,1.69166666666666,2.15));
#20802=CARTESIAN_POINT('Ctrl Pts',(0.,1.75,2.15));
#20803=CARTESIAN_POINT('Ctrl Pts',(-1.2413030787577,1.80833333333333,2.15));
#20804=CARTESIAN_POINT('Ctrl Pts',(-1.86195461813654,1.86666666666666,1.075));
#20805=CARTESIAN_POINT('Ctrl Pts',(-2.48260615751539,1.925,1.52015784217237E-16));
#20806=CARTESIAN_POINT('Ctrl Pts',(-1.86195461813654,1.98333333333333,-1.075));
#20807=CARTESIAN_POINT('Ctrl Pts',(-1.2413030787577,2.04166666666666,-2.15));
#20808=CARTESIAN_POINT('Ctrl Pts',(-2.63299061816681E-16,2.1,-2.15));
#20809=CARTESIAN_POINT('Ctrl Pts',(1.24130307875769,2.15833333333333,-2.15));
#20810=CARTESIAN_POINT('Ctrl Pts',(1.86195461813654,2.21666666666666,-1.075));
#20811=CARTESIAN_POINT('Ctrl Pts',(2.48260615751539,2.275,-4.5604735265171E-16));
#20812=CARTESIAN_POINT('Ctrl Pts',(1.86195461813654,2.33333333333333,1.075));
#20813=CARTESIAN_POINT('Ctrl Pts',(1.2413030787577,2.39166666666666,2.15));
#20814=CARTESIAN_POINT('Ctrl Pts',(0.,2.45,2.15));
#20815=CARTESIAN_POINT('Ctrl Pts',(-1.2413030787577,2.50833333333333,2.15));
#20816=CARTESIAN_POINT('Ctrl Pts',(-1.86195461813654,2.56666666666666,1.075));
#20817=CARTESIAN_POINT('Ctrl Pts',(-2.48260615751539,2.625,1.52015784217237E-16));
#20818=CARTESIAN_POINT('Ctrl Pts',(-1.86195461813654,2.68333333333333,-1.075));
#20819=CARTESIAN_POINT('Ctrl Pts',(-1.2413030787577,2.74166666666666,-2.15));
#20820=CARTESIAN_POINT('Ctrl Pts',(-2.63299061816681E-16,2.8,-2.15));
#20821=CARTESIAN_POINT('Ctrl Pts',(1.24130307875769,2.85833333333333,-2.15));
#20822=CARTESIAN_POINT('Ctrl Pts',(1.86195461813654,2.91666666666666,-1.075));
#20823=CARTESIAN_POINT('Ctrl Pts',(2.48260615751539,2.97499999999999,-4.5604735265171E-16));
#20824=CARTESIAN_POINT('Ctrl Pts',(1.86195461813654,3.03333333333333,1.075));
#20825=CARTESIAN_POINT('Ctrl Pts',(1.2413030787577,3.09166666666666,2.15));
#20826=CARTESIAN_POINT('Ctrl Pts',(0.,3.15,2.15));
#20827=CARTESIAN_POINT('Ctrl Pts',(-1.2413030787577,3.20833333333333,2.15));
#20828=CARTESIAN_POINT('Ctrl Pts',(-1.86195461813654,3.26666666666666,1.075));
#20829=CARTESIAN_POINT('Ctrl Pts',(-2.48260615751539,3.32499999999999,1.52015784217237E-16));
#20830=CARTESIAN_POINT('Ctrl Pts',(-1.86195461813654,3.38333333333333,-1.075));
#20831=CARTESIAN_POINT('Ctrl Pts',(-1.2413030787577,3.44166666666666,-2.15));
#20832=CARTESIAN_POINT('Ctrl Pts',(-2.63299061816681E-16,3.49999999999999,
-2.15));
#20833=CARTESIAN_POINT('Ctrl Pts',(1.24130307875769,3.55833333333333,-2.15));
#20834=CARTESIAN_POINT('Ctrl Pts',(1.86195461813654,3.61666666666666,-1.075));
#20835=CARTESIAN_POINT('Ctrl Pts',(2.48260615751539,3.67499999999999,-4.5604735265171E-16));
#20836=CARTESIAN_POINT('Ctrl Pts',(1.86195461813654,3.73333333333333,1.075));
#20837=CARTESIAN_POINT('Ctrl Pts',(1.2413030787577,3.79166666666666,2.15));
#20838=CARTESIAN_POINT('Ctrl Pts',(0.,3.84999999999999,2.15));
#20839=CARTESIAN_POINT('Ctrl Pts',(-1.2413030787577,3.90833333333333,2.15));
#20840=CARTESIAN_POINT('Ctrl Pts',(-1.86195461813654,3.96666666666666,1.075));
#20841=CARTESIAN_POINT('Ctrl Pts',(-2.48260615751539,4.02499999999999,1.52015784217237E-16));
#20842=CARTESIAN_POINT('Ctrl Pts',(-1.86195461813654,4.08333333333333,-1.075));
#20843=CARTESIAN_POINT('Ctrl Pts',(-1.2413030787577,4.14166666666666,-2.15));
#20844=CARTESIAN_POINT('Ctrl Pts',(-2.63299061816681E-16,4.19999999999999,
-2.15));
#20845=CARTESIAN_POINT('Ctrl Pts',(1.24130307875769,4.25833333333333,-2.15));
#20846=CARTESIAN_POINT('Ctrl Pts',(1.86195461813654,4.31666666666666,-1.075));
#20847=CARTESIAN_POINT('Ctrl Pts',(2.48260615751539,4.37499999999999,-4.5604735265171E-16));
#20848=CARTESIAN_POINT('Ctrl Pts',(1.86195461813654,4.43333333333333,1.075));
#20849=CARTESIAN_POINT('Ctrl Pts',(1.2413030787577,4.49166666666666,2.15));
#20850=CARTESIAN_POINT('Ctrl Pts',(0.,4.54999999999999,2.15));
#20851=CARTESIAN_POINT('Ctrl Pts',(0.,0.35,2.35502525316942));
#20852=CARTESIAN_POINT('Ctrl Pts',(-1.35967446386573,0.408333333333333,
2.35502525316942));
#20853=CARTESIAN_POINT('Ctrl Pts',(-2.03951169579859,0.466666666666666,
1.17751262658471));
#20854=CARTESIAN_POINT('Ctrl Pts',(-2.71934892773146,0.525,1.66512098005556E-16));
#20855=CARTESIAN_POINT('Ctrl Pts',(-2.03951169579859,0.583333333333333,
-1.17751262658471));
#20856=CARTESIAN_POINT('Ctrl Pts',(-1.35967446386573,0.641666666666666,
-2.35502525316942));
#20857=CARTESIAN_POINT('Ctrl Pts',(-2.88407413820511E-16,0.699999999999999,
-2.35502525316942));
#20858=CARTESIAN_POINT('Ctrl Pts',(1.35967446386573,0.758333333333333,-2.35502525316942));
#20859=CARTESIAN_POINT('Ctrl Pts',(2.03951169579859,0.816666666666666,-1.17751262658471));
#20860=CARTESIAN_POINT('Ctrl Pts',(2.71934892773146,0.874999999999999,-4.99536294016668E-16));
#20861=CARTESIAN_POINT('Ctrl Pts',(2.03951169579859,0.933333333333332,1.17751262658471));
#20862=CARTESIAN_POINT('Ctrl Pts',(1.35967446386573,0.991666666666665,2.35502525316942));
#20863=CARTESIAN_POINT('Ctrl Pts',(0.,1.05,2.35502525316942));
#20864=CARTESIAN_POINT('Ctrl Pts',(-1.35967446386573,1.10833333333333,2.35502525316942));
#20865=CARTESIAN_POINT('Ctrl Pts',(-2.03951169579859,1.16666666666666,1.17751262658471));
#20866=CARTESIAN_POINT('Ctrl Pts',(-2.71934892773146,1.225,1.66512098005556E-16));
#20867=CARTESIAN_POINT('Ctrl Pts',(-2.03951169579859,1.28333333333333,-1.17751262658471));
#20868=CARTESIAN_POINT('Ctrl Pts',(-1.35967446386573,1.34166666666667,-2.35502525316942));
#20869=CARTESIAN_POINT('Ctrl Pts',(-2.88407413820511E-16,1.4,-2.35502525316942));
#20870=CARTESIAN_POINT('Ctrl Pts',(1.35967446386573,1.45833333333333,-2.35502525316942));
#20871=CARTESIAN_POINT('Ctrl Pts',(2.03951169579859,1.51666666666666,-1.17751262658471));
#20872=CARTESIAN_POINT('Ctrl Pts',(2.71934892773146,1.575,-4.99536294016668E-16));
#20873=CARTESIAN_POINT('Ctrl Pts',(2.03951169579859,1.63333333333333,1.17751262658471));
#20874=CARTESIAN_POINT('Ctrl Pts',(1.35967446386573,1.69166666666666,2.35502525316942));
#20875=CARTESIAN_POINT('Ctrl Pts',(0.,1.75,2.35502525316942));
#20876=CARTESIAN_POINT('Ctrl Pts',(-1.35967446386573,1.80833333333333,2.35502525316942));
#20877=CARTESIAN_POINT('Ctrl Pts',(-2.03951169579859,1.86666666666666,1.17751262658471));
#20878=CARTESIAN_POINT('Ctrl Pts',(-2.71934892773146,1.925,1.66512098005556E-16));
#20879=CARTESIAN_POINT('Ctrl Pts',(-2.03951169579859,1.98333333333333,-1.17751262658471));
#20880=CARTESIAN_POINT('Ctrl Pts',(-1.35967446386573,2.04166666666666,-2.35502525316942));
#20881=CARTESIAN_POINT('Ctrl Pts',(-2.88407413820511E-16,2.1,-2.35502525316942));
#20882=CARTESIAN_POINT('Ctrl Pts',(1.35967446386573,2.15833333333333,-2.35502525316942));
#20883=CARTESIAN_POINT('Ctrl Pts',(2.03951169579859,2.21666666666666,-1.17751262658471));
#20884=CARTESIAN_POINT('Ctrl Pts',(2.71934892773146,2.275,-4.99536294016668E-16));
#20885=CARTESIAN_POINT('Ctrl Pts',(2.03951169579859,2.33333333333333,1.17751262658471));
#20886=CARTESIAN_POINT('Ctrl Pts',(1.35967446386573,2.39166666666666,2.35502525316942));
#20887=CARTESIAN_POINT('Ctrl Pts',(0.,2.45,2.35502525316942));
#20888=CARTESIAN_POINT('Ctrl Pts',(-1.35967446386573,2.50833333333333,2.35502525316942));
#20889=CARTESIAN_POINT('Ctrl Pts',(-2.03951169579859,2.56666666666666,1.17751262658471));
#20890=CARTESIAN_POINT('Ctrl Pts',(-2.71934892773146,2.62499999999999,1.66512098005556E-16));
#20891=CARTESIAN_POINT('Ctrl Pts',(-2.03951169579859,2.68333333333333,-1.17751262658471));
#20892=CARTESIAN_POINT('Ctrl Pts',(-1.35967446386573,2.74166666666666,-2.35502525316942));
#20893=CARTESIAN_POINT('Ctrl Pts',(-2.88407413820511E-16,2.8,-2.35502525316942));
#20894=CARTESIAN_POINT('Ctrl Pts',(1.35967446386573,2.85833333333333,-2.35502525316942));
#20895=CARTESIAN_POINT('Ctrl Pts',(2.03951169579859,2.91666666666666,-1.17751262658471));
#20896=CARTESIAN_POINT('Ctrl Pts',(2.71934892773146,2.97499999999999,-4.99536294016668E-16));
#20897=CARTESIAN_POINT('Ctrl Pts',(2.03951169579859,3.03333333333333,1.17751262658471));
#20898=CARTESIAN_POINT('Ctrl Pts',(1.35967446386573,3.09166666666666,2.35502525316942));
#20899=CARTESIAN_POINT('Ctrl Pts',(0.,3.14999999999999,2.35502525316942));
#20900=CARTESIAN_POINT('Ctrl Pts',(-1.35967446386573,3.20833333333333,2.35502525316942));
#20901=CARTESIAN_POINT('Ctrl Pts',(-2.03951169579859,3.26666666666666,1.17751262658471));
#20902=CARTESIAN_POINT('Ctrl Pts',(-2.71934892773146,3.32499999999999,1.66512098005556E-16));
#20903=CARTESIAN_POINT('Ctrl Pts',(-2.03951169579859,3.38333333333333,-1.17751262658471));
#20904=CARTESIAN_POINT('Ctrl Pts',(-1.35967446386573,3.44166666666666,-2.35502525316942));
#20905=CARTESIAN_POINT('Ctrl Pts',(-2.88407413820511E-16,3.49999999999999,
-2.35502525316942));
#20906=CARTESIAN_POINT('Ctrl Pts',(1.35967446386573,3.55833333333333,-2.35502525316942));
#20907=CARTESIAN_POINT('Ctrl Pts',(2.03951169579859,3.61666666666666,-1.17751262658471));
#20908=CARTESIAN_POINT('Ctrl Pts',(2.71934892773146,3.67499999999999,-4.99536294016668E-16));
#20909=CARTESIAN_POINT('Ctrl Pts',(2.03951169579859,3.73333333333333,1.17751262658471));
#20910=CARTESIAN_POINT('Ctrl Pts',(1.35967446386573,3.79166666666666,2.35502525316942));
#20911=CARTESIAN_POINT('Ctrl Pts',(0.,3.84999999999999,2.35502525316942));
#20912=CARTESIAN_POINT('Ctrl Pts',(-1.35967446386573,3.90833333333333,2.35502525316942));
#20913=CARTESIAN_POINT('Ctrl Pts',(-2.03951169579859,3.96666666666666,1.17751262658471));
#20914=CARTESIAN_POINT('Ctrl Pts',(-2.71934892773146,4.02499999999999,1.66512098005556E-16));
#20915=CARTESIAN_POINT('Ctrl Pts',(-2.03951169579859,4.08333333333333,-1.17751262658471));
#20916=CARTESIAN_POINT('Ctrl Pts',(-1.35967446386573,4.14166666666666,-2.35502525316942));
#20917=CARTESIAN_POINT('Ctrl Pts',(-2.88407413820511E-16,4.19999999999999,
-2.35502525316942));
#20918=CARTESIAN_POINT('Ctrl Pts',(1.35967446386573,4.25833333333332,-2.35502525316942));
#20919=CARTESIAN_POINT('Ctrl Pts',(2.03951169579859,4.31666666666666,-1.17751262658471));
#20920=CARTESIAN_POINT('Ctrl Pts',(2.71934892773146,4.37499999999999,-4.99536294016668E-16));
#20921=CARTESIAN_POINT('Ctrl Pts',(2.03951169579859,4.43333333333332,1.17751262658471));
#20922=CARTESIAN_POINT('Ctrl Pts',(1.35967446386573,4.49166666666666,2.35502525316942));
#20923=CARTESIAN_POINT('Ctrl Pts',(0.,4.54999999999999,2.35502525316942));
#20924=CARTESIAN_POINT('Ctrl Pts',(0.,0.205025253169417,2.5));
#20925=CARTESIAN_POINT('Ctrl Pts',(-1.44337567297406,0.26335858650275,2.5));
#20926=CARTESIAN_POINT('Ctrl Pts',(-2.1650635094611,0.321691919836083,1.25));
#20927=CARTESIAN_POINT('Ctrl Pts',(-2.88675134594813,0.380025253169416,
1.76762539787484E-16));
#20928=CARTESIAN_POINT('Ctrl Pts',(-2.1650635094611,0.43835858650275,-1.25));
#20929=CARTESIAN_POINT('Ctrl Pts',(-1.44337567297407,0.496691919836083,
-2.5));
#20930=CARTESIAN_POINT('Ctrl Pts',(-3.06161699786838E-16,0.555025253169416,
-2.5));
#20931=CARTESIAN_POINT('Ctrl Pts',(1.44337567297406,0.613358586502749,-2.5));
#20932=CARTESIAN_POINT('Ctrl Pts',(2.1650635094611,0.671691919836083,-1.25));
#20933=CARTESIAN_POINT('Ctrl Pts',(2.88675134594813,0.730025253169416,-5.30287619362453E-16));
#20934=CARTESIAN_POINT('Ctrl Pts',(2.1650635094611,0.788358586502749,1.25));
#20935=CARTESIAN_POINT('Ctrl Pts',(1.44337567297407,0.846691919836082,2.5));
#20936=CARTESIAN_POINT('Ctrl Pts',(0.,0.905025253169415,2.5));
#20937=CARTESIAN_POINT('Ctrl Pts',(-1.44337567297406,0.963358586502749,
2.5));
#20938=CARTESIAN_POINT('Ctrl Pts',(-2.1650635094611,1.02169191983608,1.25));
#20939=CARTESIAN_POINT('Ctrl Pts',(-2.88675134594813,1.08002525316942,1.76762539787484E-16));
#20940=CARTESIAN_POINT('Ctrl Pts',(-2.1650635094611,1.13835858650275,-1.25));
#20941=CARTESIAN_POINT('Ctrl Pts',(-1.44337567297407,1.19669191983608,-2.5));
#20942=CARTESIAN_POINT('Ctrl Pts',(-3.06161699786838E-16,1.25502525316941,
-2.5));
#20943=CARTESIAN_POINT('Ctrl Pts',(1.44337567297406,1.31335858650275,-2.5));
#20944=CARTESIAN_POINT('Ctrl Pts',(2.1650635094611,1.37169191983608,-1.25));
#20945=CARTESIAN_POINT('Ctrl Pts',(2.88675134594813,1.43002525316941,-5.30287619362453E-16));
#20946=CARTESIAN_POINT('Ctrl Pts',(2.1650635094611,1.48835858650275,1.25));
#20947=CARTESIAN_POINT('Ctrl Pts',(1.44337567297407,1.54669191983608,2.5));
#20948=CARTESIAN_POINT('Ctrl Pts',(0.,1.60502525316941,2.5));
#20949=CARTESIAN_POINT('Ctrl Pts',(-1.44337567297406,1.66335858650275,2.5));
#20950=CARTESIAN_POINT('Ctrl Pts',(-2.1650635094611,1.72169191983608,1.25));
#20951=CARTESIAN_POINT('Ctrl Pts',(-2.88675134594813,1.78002525316941,1.76762539787484E-16));
#20952=CARTESIAN_POINT('Ctrl Pts',(-2.1650635094611,1.83835858650275,-1.25));
#20953=CARTESIAN_POINT('Ctrl Pts',(-1.44337567297407,1.89669191983608,-2.5));
#20954=CARTESIAN_POINT('Ctrl Pts',(-3.06161699786838E-16,1.95502525316941,
-2.5));
#20955=CARTESIAN_POINT('Ctrl Pts',(1.44337567297406,2.01335858650275,-2.5));
#20956=CARTESIAN_POINT('Ctrl Pts',(2.1650635094611,2.07169191983608,-1.25));
#20957=CARTESIAN_POINT('Ctrl Pts',(2.88675134594813,2.13002525316941,-5.30287619362453E-16));
#20958=CARTESIAN_POINT('Ctrl Pts',(2.1650635094611,2.18835858650275,1.25));
#20959=CARTESIAN_POINT('Ctrl Pts',(1.44337567297407,2.24669191983608,2.5));
#20960=CARTESIAN_POINT('Ctrl Pts',(0.,2.30502525316941,2.5));
#20961=CARTESIAN_POINT('Ctrl Pts',(-1.44337567297406,2.36335858650275,2.5));
#20962=CARTESIAN_POINT('Ctrl Pts',(-2.1650635094611,2.42169191983608,1.25));
#20963=CARTESIAN_POINT('Ctrl Pts',(-2.88675134594813,2.48002525316941,1.76762539787484E-16));
#20964=CARTESIAN_POINT('Ctrl Pts',(-2.1650635094611,2.53835858650275,-1.25));
#20965=CARTESIAN_POINT('Ctrl Pts',(-1.44337567297407,2.59669191983608,-2.5));
#20966=CARTESIAN_POINT('Ctrl Pts',(-3.06161699786838E-16,2.65502525316941,
-2.5));
#20967=CARTESIAN_POINT('Ctrl Pts',(1.44337567297406,2.71335858650274,-2.5));
#20968=CARTESIAN_POINT('Ctrl Pts',(2.1650635094611,2.77169191983608,-1.25));
#20969=CARTESIAN_POINT('Ctrl Pts',(2.88675134594813,2.83002525316941,-5.30287619362453E-16));
#20970=CARTESIAN_POINT('Ctrl Pts',(2.1650635094611,2.88835858650274,1.25));
#20971=CARTESIAN_POINT('Ctrl Pts',(1.44337567297407,2.94669191983608,2.5));
#20972=CARTESIAN_POINT('Ctrl Pts',(0.,3.00502525316941,2.5));
#20973=CARTESIAN_POINT('Ctrl Pts',(-1.44337567297406,3.06335858650274,2.5));
#20974=CARTESIAN_POINT('Ctrl Pts',(-2.1650635094611,3.12169191983608,1.25));
#20975=CARTESIAN_POINT('Ctrl Pts',(-2.88675134594813,3.18002525316941,1.76762539787484E-16));
#20976=CARTESIAN_POINT('Ctrl Pts',(-2.1650635094611,3.23835858650274,-1.25));
#20977=CARTESIAN_POINT('Ctrl Pts',(-1.44337567297407,3.29669191983608,-2.5));
#20978=CARTESIAN_POINT('Ctrl Pts',(-3.06161699786838E-16,3.35502525316941,
-2.5));
#20979=CARTESIAN_POINT('Ctrl Pts',(1.44337567297406,3.41335858650274,-2.5));
#20980=CARTESIAN_POINT('Ctrl Pts',(2.1650635094611,3.47169191983608,-1.25));
#20981=CARTESIAN_POINT('Ctrl Pts',(2.88675134594813,3.53002525316941,-5.30287619362453E-16));
#20982=CARTESIAN_POINT('Ctrl Pts',(2.1650635094611,3.58835858650274,1.25));
#20983=CARTESIAN_POINT('Ctrl Pts',(1.44337567297407,3.64669191983608,2.5));
#20984=CARTESIAN_POINT('Ctrl Pts',(0.,3.70502525316941,2.5));
#20985=CARTESIAN_POINT('Ctrl Pts',(-1.44337567297406,3.76335858650274,2.5));
#20986=CARTESIAN_POINT('Ctrl Pts',(-2.1650635094611,3.82169191983608,1.25));
#20987=CARTESIAN_POINT('Ctrl Pts',(-2.88675134594813,3.88002525316941,1.76762539787484E-16));
#20988=CARTESIAN_POINT('Ctrl Pts',(-2.1650635094611,3.93835858650274,-1.25));
#20989=CARTESIAN_POINT('Ctrl Pts',(-1.44337567297407,3.99669191983608,-2.5));
#20990=CARTESIAN_POINT('Ctrl Pts',(-3.06161699786838E-16,4.05502525316941,
-2.5));
#20991=CARTESIAN_POINT('Ctrl Pts',(1.44337567297406,4.11335858650274,-2.5));
#20992=CARTESIAN_POINT('Ctrl Pts',(2.1650635094611,4.17169191983608,-1.25));
#20993=CARTESIAN_POINT('Ctrl Pts',(2.88675134594813,4.23002525316941,-5.30287619362453E-16));
#20994=CARTESIAN_POINT('Ctrl Pts',(2.1650635094611,4.28835858650274,1.25));
#20995=CARTESIAN_POINT('Ctrl Pts',(1.44337567297407,4.34669191983608,2.5));
#20996=CARTESIAN_POINT('Ctrl Pts',(0.,4.40502525316941,2.5));
#20997=CARTESIAN_POINT('Ctrl Pts',(0.,4.28626379701574E-17,2.5));
#20998=CARTESIAN_POINT('Ctrl Pts',(-1.44337567297406,0.0583333333333333,
2.5));
#20999=CARTESIAN_POINT('Ctrl Pts',(-2.1650635094611,0.116666666666666,1.25));
#21000=CARTESIAN_POINT('Ctrl Pts',(-2.88675134594813,0.175,1.76762539787484E-16));
#21001=CARTESIAN_POINT('Ctrl Pts',(-2.1650635094611,0.233333333333333,-1.25));
#21002=CARTESIAN_POINT('Ctrl Pts',(-1.44337567297407,0.291666666666666,
-2.5));
#21003=CARTESIAN_POINT('Ctrl Pts',(-3.06161699786838E-16,0.349999999999999,
-2.5));
#21004=CARTESIAN_POINT('Ctrl Pts',(1.44337567297406,0.408333333333333,-2.5));
#21005=CARTESIAN_POINT('Ctrl Pts',(2.1650635094611,0.466666666666666,-1.25));
#21006=CARTESIAN_POINT('Ctrl Pts',(2.88675134594813,0.524999999999999,-5.30287619362453E-16));
#21007=CARTESIAN_POINT('Ctrl Pts',(2.1650635094611,0.583333333333332,1.25));
#21008=CARTESIAN_POINT('Ctrl Pts',(1.44337567297407,0.641666666666665,2.5));
#21009=CARTESIAN_POINT('Ctrl Pts',(0.,0.699999999999999,2.5));
#21010=CARTESIAN_POINT('Ctrl Pts',(-1.44337567297406,0.758333333333332,
2.5));
#21011=CARTESIAN_POINT('Ctrl Pts',(-2.1650635094611,0.816666666666665,1.25));
#21012=CARTESIAN_POINT('Ctrl Pts',(-2.88675134594813,0.874999999999998,
1.76762539787484E-16));
#21013=CARTESIAN_POINT('Ctrl Pts',(-2.1650635094611,0.933333333333332,-1.25));
#21014=CARTESIAN_POINT('Ctrl Pts',(-1.44337567297407,0.991666666666665,
-2.5));
#21015=CARTESIAN_POINT('Ctrl Pts',(-3.06161699786838E-16,1.05,-2.5));
#21016=CARTESIAN_POINT('Ctrl Pts',(1.44337567297406,1.10833333333333,-2.5));
#21017=CARTESIAN_POINT('Ctrl Pts',(2.1650635094611,1.16666666666666,-1.25));
#21018=CARTESIAN_POINT('Ctrl Pts',(2.88675134594813,1.225,-5.30287619362453E-16));
#21019=CARTESIAN_POINT('Ctrl Pts',(2.1650635094611,1.28333333333333,1.25));
#21020=CARTESIAN_POINT('Ctrl Pts',(1.44337567297407,1.34166666666666,2.5));
#21021=CARTESIAN_POINT('Ctrl Pts',(0.,1.4,2.5));
#21022=CARTESIAN_POINT('Ctrl Pts',(-1.44337567297406,1.45833333333333,2.5));
#21023=CARTESIAN_POINT('Ctrl Pts',(-2.1650635094611,1.51666666666666,1.25));
#21024=CARTESIAN_POINT('Ctrl Pts',(-2.88675134594813,1.575,1.76762539787484E-16));
#21025=CARTESIAN_POINT('Ctrl Pts',(-2.1650635094611,1.63333333333333,-1.25));
#21026=CARTESIAN_POINT('Ctrl Pts',(-1.44337567297407,1.69166666666666,-2.5));
#21027=CARTESIAN_POINT('Ctrl Pts',(-3.06161699786838E-16,1.75,-2.5));
#21028=CARTESIAN_POINT('Ctrl Pts',(1.44337567297406,1.80833333333333,-2.5));
#21029=CARTESIAN_POINT('Ctrl Pts',(2.1650635094611,1.86666666666666,-1.25));
#21030=CARTESIAN_POINT('Ctrl Pts',(2.88675134594813,1.925,-5.30287619362453E-16));
#21031=CARTESIAN_POINT('Ctrl Pts',(2.1650635094611,1.98333333333333,1.25));
#21032=CARTESIAN_POINT('Ctrl Pts',(1.44337567297407,2.04166666666666,2.5));
#21033=CARTESIAN_POINT('Ctrl Pts',(0.,2.1,2.5));
#21034=CARTESIAN_POINT('Ctrl Pts',(-1.44337567297406,2.15833333333333,2.5));
#21035=CARTESIAN_POINT('Ctrl Pts',(-2.1650635094611,2.21666666666666,1.25));
#21036=CARTESIAN_POINT('Ctrl Pts',(-2.88675134594813,2.275,1.76762539787484E-16));
#21037=CARTESIAN_POINT('Ctrl Pts',(-2.1650635094611,2.33333333333333,-1.25));
#21038=CARTESIAN_POINT('Ctrl Pts',(-1.44337567297407,2.39166666666666,-2.5));
#21039=CARTESIAN_POINT('Ctrl Pts',(-3.06161699786838E-16,2.45,-2.5));
#21040=CARTESIAN_POINT('Ctrl Pts',(1.44337567297406,2.50833333333333,-2.5));
#21041=CARTESIAN_POINT('Ctrl Pts',(2.1650635094611,2.56666666666666,-1.25));
#21042=CARTESIAN_POINT('Ctrl Pts',(2.88675134594813,2.62499999999999,-5.30287619362453E-16));
#21043=CARTESIAN_POINT('Ctrl Pts',(2.1650635094611,2.68333333333333,1.25));
#21044=CARTESIAN_POINT('Ctrl Pts',(1.44337567297407,2.74166666666666,2.5));
#21045=CARTESIAN_POINT('Ctrl Pts',(0.,2.79999999999999,2.5));
#21046=CARTESIAN_POINT('Ctrl Pts',(-1.44337567297406,2.85833333333333,2.5));
#21047=CARTESIAN_POINT('Ctrl Pts',(-2.1650635094611,2.91666666666666,1.25));
#21048=CARTESIAN_POINT('Ctrl Pts',(-2.88675134594813,2.97499999999999,1.76762539787484E-16));
#21049=CARTESIAN_POINT('Ctrl Pts',(-2.1650635094611,3.03333333333333,-1.25));
#21050=CARTESIAN_POINT('Ctrl Pts',(-1.44337567297407,3.09166666666666,-2.5));
#21051=CARTESIAN_POINT('Ctrl Pts',(-3.06161699786838E-16,3.14999999999999,
-2.5));
#21052=CARTESIAN_POINT('Ctrl Pts',(1.44337567297406,3.20833333333333,-2.5));
#21053=CARTESIAN_POINT('Ctrl Pts',(2.1650635094611,3.26666666666666,-1.25));
#21054=CARTESIAN_POINT('Ctrl Pts',(2.88675134594813,3.32499999999999,-5.30287619362453E-16));
#21055=CARTESIAN_POINT('Ctrl Pts',(2.1650635094611,3.38333333333333,1.25));
#21056=CARTESIAN_POINT('Ctrl Pts',(1.44337567297407,3.44166666666666,2.5));
#21057=CARTESIAN_POINT('Ctrl Pts',(0.,3.49999999999999,2.5));
#21058=CARTESIAN_POINT('Ctrl Pts',(-1.44337567297406,3.55833333333333,2.5));
#21059=CARTESIAN_POINT('Ctrl Pts',(-2.1650635094611,3.61666666666666,1.25));
#21060=CARTESIAN_POINT('Ctrl Pts',(-2.88675134594813,3.67499999999999,1.76762539787484E-16));
#21061=CARTESIAN_POINT('Ctrl Pts',(-2.1650635094611,3.73333333333333,-1.25));
#21062=CARTESIAN_POINT('Ctrl Pts',(-1.44337567297407,3.79166666666666,-2.5));
#21063=CARTESIAN_POINT('Ctrl Pts',(-3.06161699786838E-16,3.84999999999999,
-2.5));
#21064=CARTESIAN_POINT('Ctrl Pts',(1.44337567297406,3.90833333333333,-2.5));
#21065=CARTESIAN_POINT('Ctrl Pts',(2.1650635094611,3.96666666666666,-1.25));
#21066=CARTESIAN_POINT('Ctrl Pts',(2.88675134594813,4.02499999999999,-5.30287619362453E-16));
#21067=CARTESIAN_POINT('Ctrl Pts',(2.1650635094611,4.08333333333333,1.25));
#21068=CARTESIAN_POINT('Ctrl Pts',(1.44337567297407,4.14166666666666,2.5));
#21069=CARTESIAN_POINT('Ctrl Pts',(0.,4.19999999999999,2.5));
#21070=CARTESIAN_POINT('Origin',(0.,0.,2.15));
#21071=CARTESIAN_POINT('Origin',(-1.80160437084306E-13,4.2,2.15));
#21072=CARTESIAN_POINT('Origin',(-1.80160437084306E-13,4.2,2.15));
#21073=CARTESIAN_POINT('Origin',(0.,0.,2.15));
#32961=UNCERTAINTY_MEASURE_WITH_UNIT(LENGTH_MEASURE(0.01),#33017,
'DISTANCE_ACCURACY_VALUE',
'Maximum model space distance between geometric entities at asserted c
onnectivities');
#32984=UNCERTAINTY_MEASURE_WITH_UNIT(LENGTH_MEASURE(0.01),#33017,
'DISTANCE_ACCURACY_VALUE',
'Maximum model space distance between geometric entities at asserted c
onnectivities');
#32993=(
GEOMETRIC_REPRESENTATION_CONTEXT(3)
GLOBAL_UNCERTAINTY_ASSIGNED_CONTEXT((#32961))
GLOBAL_UNIT_ASSIGNED_CONTEXT((#33017,#33019,#33020))
REPRESENTATION_CONTEXT('','3D')
);
#33016=(
GEOMETRIC_REPRESENTATION_CONTEXT(3)
GLOBAL_UNCERTAINTY_ASSIGNED_CONTEXT((#32984))
GLOBAL_UNIT_ASSIGNED_CONTEXT((#33017,#33019,#33020))
REPRESENTATION_CONTEXT('','3D')
);
#33017=(
LENGTH_UNIT()
NAMED_UNIT(*)
SI_UNIT(.MILLI.,.METRE.)
);
#33019=(
NAMED_UNIT(*)
PLANE_ANGLE_UNIT()
SI_UNIT($,.RADIAN.)
);
#33020=(
NAMED_UNIT(*)
SI_UNIT($,.STERADIAN.)
SOLID_ANGLE_UNIT()
);
#33029=SHAPE_DEFINITION_REPRESENTATION(#33060,#33132);
#33060=PRODUCT_DEFINITION_SHAPE('',$,#33164);
#33132=SHAPE_REPRESENTATION('',(#10677),#32993);
#33155=PRODUCT_DEFINITION_CONTEXT('part definition',#33250,'design');
#33164=PRODUCT_DEFINITION(
'BO21-002_Spring_PUR-HW-4008_0.7x5x10_M_Rev00 (C)','PUR-HW-4008',#33195,
#33155);
#33195=PRODUCT_DEFINITION_FORMATION('',$,#33260);
#33250=APPLICATION_CONTEXT(
'Core Data for Automotive Mechanical Design Process');
#33251=PRODUCT_CONTEXT('part definition',#33250,'mechanical');
#33260=PRODUCT('BO21-002_Spring_PUR-HW-4008_0.7x5x10_M_Rev00 (C)',
'PUR-HW-4008',$,(#33251));
#33285=PRESENTATION_STYLE_ASSIGNMENT((#33292));
#33292=SURFACE_STYLE_USAGE(.BOTH.,#33299);
#33299=SURFACE_SIDE_STYLE('',(#33306));
#33306=SURFACE_STYLE_FILL_AREA(#33313);
#33313=FILL_AREA_STYLE('Opaque(202,209,238)',(#33320));
#33320=FILL_AREA_STYLE_COLOUR('Opaque(202,209,238)',#33327);
#33327=COLOUR_RGB('Opaque(202,209,238)', 0.08235294, 0.09019608, 0.10196078);
ENDSEC;
END-ISO-10303-21;
